ISO-10303-21;
HEADER;
FILE_DESCRIPTION (('STEP AP214'),
    '1' );
FILE_NAME ('base.step',
    '2026-10-08T12:12:07',
    ( '' ),
    ( '' ),
    'SwSTEP 2.0',
    'SolidWorks 2026',
    '' );
FILE_SCHEMA (( 'AUTOMOTIVE_DESIGN' ));
ENDSEC;

DATA;
#2=DIRECTION ( 'NONE',  ( -0.000000000000000000, -0.000000000000000000, -1.000000000000000000 ) ) ;
#7=CARTESIAN_POINT ( 'NONE',  ( -34.99999999999999289, 30.00000000000000711, 10.00000000000000000 ) ) ;
#18=CARTESIAN_POINT ( 'NONE',  ( -10.00000000000000000, 0.000000000000000000, 18.00000000000000355 ) ) ;
#27=CARTESIAN_POINT ( 'NONE',  ( 29.99999999999997868, 30.00000000000001421, 10.00000000000000000 ) ) ;
#29=DIRECTION ( 'NONE',  ( 1.000000000000000000, 0.000000000000000000, 0.000000000000000000 ) ) ;
#30=CARTESIAN_POINT ( 'NONE',  ( 29.99999999999997868, 30.00000000000001421, 10.00000000000000000 ) ) ;
#41=EDGE_LOOP ( 'NONE', ( #7482, #4970, #5659, #4712 ) ) ;
#46=FACE_OUTER_BOUND ( 'NONE', #941, .T. ) ;
#52=ADVANCED_FACE ( 'NONE', ( #6515 ), #2195, .F. ) ;
#77=AXIS2_PLACEMENT_3D ( 'NONE', #6782, #2260, #420 ) ;
#82=EDGE_CURVE ( 'NONE', #4888, #7000, #5116, .T. ) ;
#97=DIRECTION ( 'NONE',  ( 1.000000000000000000, 0.000000000000000000, 0.000000000000000000 ) ) ;
#101=DIRECTION ( 'NONE',  ( -1.000000000000000000, 0.000000000000000000, 0.000000000000000000 ) ) ;
#109=PRESENTATION_STYLE_ASSIGNMENT (( #7641 ) ) ;
#123=ORIENTED_EDGE ( 'NONE', *, *, #702, .T. ) ;
#133=VECTOR ( 'NONE', #5005, 1000.000000000000000 ) ;
#137=FACE_OUTER_BOUND ( 'NONE', #4836, .T. ) ;
#143=DIRECTION ( 'NONE',  ( -0.000000000000000000, -0.000000000000000000, 1.000000000000000000 ) ) ;
#154=DIRECTION ( 'NONE',  ( 1.000000000000000000, 0.000000000000000000, 0.000000000000000000 ) ) ;
#157=VERTEX_POINT ( 'NONE', #7474 ) ;
#159=EDGE_LOOP ( 'NONE', ( #4491, #1533, #7142, #8130 ) ) ;
#169=UNCERTAINTY_MEASURE_WITH_UNIT (LENGTH_MEASURE( 1.000000000000000082E-05 ), #2071, 'distance_accuracy_value', 'NONE');
#180=CARTESIAN_POINT ( 'NONE',  ( -34.99999999999999289, -29.99999999999999289, 4.599999999999997868 ) ) ;
#191=VERTEX_POINT ( 'NONE', #2408 ) ;
#194=CARTESIAN_POINT ( 'NONE',  ( -24.99999999999999645, 30.00000000000000711, 10.00000000000000000 ) ) ;
#219=DIRECTION ( 'NONE',  ( -0.000000000000000000, -0.000000000000000000, 1.000000000000000000 ) ) ;
#232=AXIS2_PLACEMENT_3D ( 'NONE', #857, #2671, #5216 ) ;
#238=VECTOR ( 'NONE', #7982, 1000.000000000000000 ) ;
#245=AXIS2_PLACEMENT_3D ( 'NONE', #8189, #4513, #2470 ) ;
#246=DIRECTION ( 'NONE',  ( 1.000000000000000000, 0.000000000000000000, 0.000000000000000000 ) ) ;
#252=AXIS2_PLACEMENT_3D ( 'NONE', #5711, #1219, #3844 ) ;
#256=AXIS2_PLACEMENT_3D ( 'NONE', #3380, #1548, #4591 ) ;
#264=CARTESIAN_POINT ( 'NONE',  ( 25.00000000000001421, -29.99999999999997868, 4.599999999999997868 ) ) ;
#267=FACE_OUTER_BOUND ( 'NONE', #3148, .T. ) ;
#271=EDGE_CURVE ( 'NONE', #3838, #583, #4171, .T. ) ;
#272=ORIENTED_EDGE ( 'NONE', *, *, #404, .T. ) ;
#276=DIRECTION ( 'NONE',  ( 1.000000000000000000, 0.000000000000000000, 0.000000000000000000 ) ) ;
#314=VERTEX_POINT ( 'NONE', #7605 ) ;
#316=DIRECTION ( 'NONE',  ( 1.000000000000000000, 0.000000000000000000, 0.000000000000000000 ) ) ;
#326=CYLINDRICAL_SURFACE ( 'NONE', #7568, 2.649999999999999467 ) ;
#330=ORIENTED_EDGE ( 'NONE', *, *, #3696, .T. ) ;
#332=CARTESIAN_POINT ( 'NONE',  ( 2.650000000000010125, 3.245314017740498288E-16, 5.400000000000002132 ) ) ;
#336=CARTESIAN_POINT ( 'NONE',  ( -4.999999999999993783, 0.000000000000000000, 3.851859888774471706E-31 ) ) ;
#346=DIRECTION ( 'NONE',  ( 1.000000000000000000, 0.000000000000000000, 0.000000000000000000 ) ) ;
#371=CIRCLE ( 'NONE', #3847, 7.000000000000000000 ) ;
#372=AXIS2_PLACEMENT_3D ( 'NONE', #7047, #966, #5953 ) ;
#379=CYLINDRICAL_SURFACE ( 'NONE', #4378, 2.649999999999999467 ) ;
#387=ORIENTED_EDGE ( 'NONE', *, *, #1940, .F. ) ;
#393=DIRECTION ( 'NONE',  ( 1.000000000000000000, 0.000000000000000000, 0.000000000000000000 ) ) ;
#401=ADVANCED_FACE ( 'NONE', ( #1245, #7092 ), #6269, .F. ) ;
#402=VERTEX_POINT ( 'NONE', #4485 ) ;
#404=EDGE_CURVE ( 'NONE', #1899, #4446, #4447, .T. ) ;
#412=ORIENTED_EDGE ( 'NONE', *, *, #702, .F. ) ;
#420=DIRECTION ( 'NONE',  ( 0.000000000000000000, 0.000000000000000000, 1.000000000000000000 ) ) ;
#430=ORIENTED_EDGE ( 'NONE', *, *, #3127, .T. ) ;
#437=DIRECTION ( 'NONE',  ( 1.000000000000000000, 0.000000000000000000, 0.000000000000000000 ) ) ;
#446=CARTESIAN_POINT ( 'NONE',  ( -29.99999999999999289, 30.00000000000000711, 1.734723475976807094E-15 ) ) ;
#451=EDGE_LOOP ( 'NONE', ( #6114, #5624, #2081, #2869 ) ) ;
#453=ORIENTED_EDGE ( 'NONE', *, *, #6162, .T. ) ;
#457=EDGE_CURVE ( 'NONE', #4563, #191, #2069, .T. ) ;
#461=EDGE_LOOP ( 'NONE', ( #4654, #4669, #5460, #5904 ) ) ;
#469=CARTESIAN_POINT ( 'NONE',  ( 30.00000000000001066, -29.99999999999997868, 10.00000000000000000 ) ) ;
#477=CARTESIAN_POINT ( 'NONE',  ( 29.99999999999997868, 30.00000000000001421, 4.599999999999997868 ) ) ;
#484=CARTESIAN_POINT ( 'NONE',  ( 0.000000000000000000, 0.000000000000000000, 10.00000000000000000 ) ) ;
#489=ORIENTED_EDGE ( 'NONE', *, *, #82, .F. ) ;
#490=EDGE_LOOP ( 'NONE', ( #4161, #8112 ) ) ;
#506=EDGE_LOOP ( 'NONE', ( #7352, #658 ) ) ;
#510=AXIS2_PLACEMENT_3D ( 'NONE', #2860, #987, #5527 ) ;
#512=CARTESIAN_POINT ( 'NONE',  ( -27.34999999999999076, 30.00000000000000711, 10.00000000000000000 ) ) ;
#514=DIRECTION ( 'NONE',  ( -0.000000000000000000, -0.000000000000000000, 1.000000000000000000 ) ) ;
#517=( GEOMETRIC_REPRESENTATION_CONTEXT ( 3 ) GLOBAL_UNCERTAINTY_ASSIGNED_CONTEXT ( ( #1718 ) ) GLOBAL_UNIT_ASSIGNED_CONTEXT ( ( #4596, #2718, #1440 ) ) REPRESENTATION_CONTEXT ( 'NONE', 'WORKASPACE' ) );
#519=ORIENTED_EDGE ( 'NONE', *, *, #7020, .F. ) ;
#525=AXIS2_PLACEMENT_3D ( 'NONE', #4973, #3598, #1680 ) ;
#536=DIRECTION ( 'NONE',  ( 0.000000000000000000, 0.000000000000000000, 1.000000000000000000 ) ) ;
#563=ORIENTED_EDGE ( 'NONE', *, *, #7710, .T. ) ;
#565=CYLINDRICAL_SURFACE ( 'NONE', #881, 2.650000000000003020 ) ;
#583=VERTEX_POINT ( 'NONE', #883 ) ;
#590=VERTEX_POINT ( 'NONE', #6040 ) ;
#595=FACE_BOUND ( 'NONE', #8029, .T. ) ;
#596=EDGE_CURVE ( 'NONE', #8175, #5459, #6549, .T. ) ;
#598=DIRECTION ( 'NONE',  ( 1.000000000000000000, 0.000000000000000000, 0.000000000000000000 ) ) ;
#602=FACE_OUTER_BOUND ( 'NONE', #1472, .T. ) ;
#605=FACE_OUTER_BOUND ( 'NONE', #2156, .T. ) ;
#607=DIRECTION ( 'NONE',  ( -0.000000000000000000, -0.000000000000000000, -1.000000000000000000 ) ) ;
#613=CARTESIAN_POINT ( 'NONE',  ( -39.99999999999999289, -39.99999999999999289, 0.000000000000000000 ) ) ;
#621=EDGE_CURVE ( 'NONE', #5625, #2558, #2116, .T. ) ;
#624=ORIENTED_EDGE ( 'NONE', *, *, #3897, .T. ) ;
#642=VECTOR ( 'NONE', #6144, 1000.000000000000000 ) ;
#652=VECTOR ( 'NONE', #7598, 1000.000000000000000 ) ;
#658=ORIENTED_EDGE ( 'NONE', *, *, #5836, .T. ) ;
#671=EDGE_LOOP ( 'NONE', ( #7354, #3474, #1161, #4159 ) ) ;
#675=CIRCLE ( 'NONE', #1739, 2.649999999999995914 ) ;
#678=CARTESIAN_POINT ( 'NONE',  ( 0.000000000000000000, 0.000000000000000000, 0.000000000000000000 ) ) ;
#688=DIRECTION ( 'NONE',  ( 1.000000000000000000, 0.000000000000000000, 0.000000000000000000 ) ) ;
#690=CARTESIAN_POINT ( 'NONE',  ( -29.99999999999999289, 30.00000000000000711, 4.599999999999997868 ) ) ;
#691=CARTESIAN_POINT ( 'NONE',  ( -39.99999999999999289, -39.99999999999999289, 10.00000000000000000 ) ) ;
#699=DIRECTION ( 'NONE',  ( 1.000000000000000000, 0.000000000000000000, 0.000000000000000000 ) ) ;
#702=EDGE_CURVE ( 'NONE', #4465, #4618, #5706, .T. ) ;
#706=EDGE_CURVE ( 'NONE', #583, #3838, #786, .T. ) ;
#707=DIRECTION ( 'NONE',  ( 1.000000000000000000, 0.000000000000000000, 0.000000000000000000 ) ) ;
#708=VERTEX_POINT ( 'NONE', #1382 ) ;
#719=CARTESIAN_POINT ( 'NONE',  ( 32.65000000000000568, -29.99999999999997868, 1.734723475976807094E-15 ) ) ;
#728=CARTESIAN_POINT ( 'NONE',  ( 32.65000000000000568, -29.99999999999997868, 4.599999999999997868 ) ) ;
#730=ORIENTED_EDGE ( 'NONE', *, *, #457, .F. ) ;
#739=DIRECTION ( 'NONE',  ( -0.000000000000000000, -0.000000000000000000, 1.000000000000000000 ) ) ;
#749=FACE_BOUND ( 'NONE', #8022, .T. ) ;
#757=DIRECTION ( 'NONE',  ( -0.000000000000000000, -0.000000000000000000, 1.000000000000000000 ) ) ;
#763=AXIS2_PLACEMENT_3D ( 'NONE', #949, #2245, #5530 ) ;
#767=APPLICATION_CONTEXT ( 'automotive_design' ) ;
#768=FILL_AREA_STYLE ('',( #5810 ) ) ;
#772=CYLINDRICAL_SURFACE ( 'NONE', #7542, 4.999999999999993783 ) ;
#777=ORIENTED_EDGE ( 'NONE', *, *, #3974, .F. ) ;
#786=CIRCLE ( 'NONE', #2249, 2.649999999999999467 ) ;
#788=CYLINDRICAL_SURFACE ( 'NONE', #7291, 4.999999999999993783 ) ;
#792=VERTEX_POINT ( 'NONE', #4851 ) ;
#794=ORIENTED_EDGE ( 'NONE', *, *, #1343, .T. ) ;
#808=ORIENTED_EDGE ( 'NONE', *, *, #8120, .F. ) ;
#809=CARTESIAN_POINT ( 'NONE',  ( -27.35000000000000497, -29.99999999999999289, 10.00000000000000000 ) ) ;
#828=ORIENTED_EDGE ( 'NONE', *, *, #706, .T. ) ;
#853=CARTESIAN_POINT ( 'NONE',  ( 27.34999999999998010, 30.00000000000001421, 10.00000000000000000 ) ) ;
#857=CARTESIAN_POINT ( 'NONE',  ( -27.35000000000000142, -29.99999999999999289, 4.599999999999997868 ) ) ;
#858=DIRECTION ( 'NONE',  ( 1.000000000000000000, 0.000000000000000000, 0.000000000000000000 ) ) ;
#861=EDGE_LOOP ( 'NONE', ( #1217, #2447 ) ) ;
#862=ORIENTED_EDGE ( 'NONE', *, *, #1211, .T. ) ;
#866=CARTESIAN_POINT ( 'NONE',  ( 29.99999999999997868, 30.00000000000001421, 10.00000000000000000 ) ) ;
#877=ADVANCED_FACE ( 'NONE', ( #1694 ), #7995, .F. ) ;
#881=AXIS2_PLACEMENT_3D ( 'NONE', #5603, #3643, #1102 ) ;
#883=CARTESIAN_POINT ( 'NONE',  ( 27.34999999999998010, 30.00000000000001421, 1.734723475976807094E-15 ) ) ;
#892=CARTESIAN_POINT ( 'NONE',  ( 0.000000000000000000, 0.000000000000000000, 5.400000000000002132 ) ) ;
#920=EDGE_CURVE ( 'NONE', #4585, #1494, #2000, .T. ) ;
#934=CARTESIAN_POINT ( 'NONE',  ( -10.00000000000000000, 0.000000000000000000, 18.00000000000000355 ) ) ;
#941=EDGE_LOOP ( 'NONE', ( #412, #6401, #3522, #5747 ) ) ;
#944=CARTESIAN_POINT ( 'NONE',  ( -29.99999999999999289, 30.00000000000000711, 4.599999999999997868 ) ) ;
#949=CARTESIAN_POINT ( 'NONE',  ( -30.00000000000000355, -29.99999999999999289, 1.734723475976807094E-15 ) ) ;
#955=ORIENTED_EDGE ( 'NONE', *, *, #3106, .T. ) ;
#966=DIRECTION ( 'NONE',  ( -0.000000000000000000, -0.000000000000000000, -1.000000000000000000 ) ) ;
#968=EDGE_CURVE ( 'NONE', #5998, #314, #7168, .T. ) ;
#975=CARTESIAN_POINT ( 'NONE',  ( -7.000000000000000000, 0.000000000000000000, 18.00000000000000355 ) ) ;
#987=DIRECTION ( 'NONE',  ( 0.000000000000000000, 0.000000000000000000, 1.000000000000000000 ) ) ;
#1004=ADVANCED_FACE ( 'NONE', ( #4443, #3319 ), #1327, .F. ) ;
#1006=VECTOR ( 'NONE', #3517, 1000.000000000000000 ) ;
#1023=ORIENTED_EDGE ( 'NONE', *, *, #4321, .F. ) ;
#1036=EDGE_LOOP ( 'NONE', ( #4205, #862, #2315, #3701 ) ) ;
#1038=VERTEX_POINT ( 'NONE', #1283 ) ;
#1041=CARTESIAN_POINT ( 'NONE',  ( -25.00000000000000711, -29.99999999999999289, 4.599999999999997868 ) ) ;
#1052=CARTESIAN_POINT ( 'NONE',  ( -39.99999999999999289, -39.99999999999999289, 10.00000000000000000 ) ) ;
#1053=ADVANCED_FACE ( 'NONE', ( #1996 ), #7051, .F. ) ;
#1055=PRODUCT_DEFINITION_SHAPE ( 'NONE', 'NONE',  #1782 ) ;
#1072=EDGE_CURVE ( 'NONE', #5459, #8175, #5974, .T. ) ;
#1090=ORIENTED_EDGE ( 'NONE', *, *, #4303, .F. ) ;
#1097=EDGE_CURVE ( 'NONE', #6822, #157, #3510, .T. ) ;
#1100=ORIENTED_EDGE ( 'NONE', *, *, #1276, .T. ) ;
#1102=DIRECTION ( 'NONE',  ( -1.000000000000000000, 0.000000000000000000, 0.000000000000000000 ) ) ;
#1104=DIRECTION ( 'NONE',  ( 1.000000000000000000, 0.000000000000000000, 0.000000000000000000 ) ) ;
#1120=EDGE_LOOP ( 'NONE', ( #2459, #4178 ) ) ;
#1130=EDGE_LOOP ( 'NONE', ( #3957, #6831, #3928, #2663 ) ) ;
#1137=EDGE_CURVE ( 'NONE', #4618, #3296, #6387, .T. ) ;
#1150=DIRECTION ( 'NONE',  ( -1.000000000000000000, 0.000000000000000000, -0.000000000000000000 ) ) ;
#1154=LINE ( 'NONE', #4956, #4353 ) ;
#1156=VERTEX_POINT ( 'NONE', #336 ) ;
#1161=ORIENTED_EDGE ( 'NONE', *, *, #6259, .T. ) ;
#1165=AXIS2_PLACEMENT_3D ( 'NONE', #3394, #6464, #1339 ) ;
#1166=DIRECTION ( 'NONE',  ( 0.000000000000000000, -0.000000000000000000, -1.000000000000000000 ) ) ;
#1167=CARTESIAN_POINT ( 'NONE',  ( 27.35000000000001208, -29.99999999999997868, 4.599999999999997868 ) ) ;
#1173=ORIENTED_EDGE ( 'NONE', *, *, #5153, .T. ) ;
#1177=AXIS2_PLACEMENT_3D ( 'NONE', #2685, #7712, #2029 ) ;
#1186=AXIS2_PLACEMENT_3D ( 'NONE', #2421, #6065, #4328 ) ;
#1194=DIRECTION ( 'NONE',  ( -0.000000000000000000, -1.000000000000000000, -0.000000000000000000 ) ) ;
#1198=AXIS2_PLACEMENT_3D ( 'NONE', #6345, #1824, #3155 ) ;
#1211=EDGE_CURVE ( 'NONE', #2407, #6822, #7828, .T. ) ;
#1217=ORIENTED_EDGE ( 'NONE', *, *, #2136, .T. ) ;
#1219=DIRECTION ( 'NONE',  ( -0.000000000000000000, -0.000000000000000000, 1.000000000000000000 ) ) ;
#1224=ORIENTED_EDGE ( 'NONE', *, *, #6422, .F. ) ;
#1226=DIRECTION ( 'NONE',  ( 1.000000000000000000, 0.000000000000000000, 0.000000000000000000 ) ) ;
#1234=ORIENTED_EDGE ( 'NONE', *, *, #4481, .F. ) ;
#1239=CYLINDRICAL_SURFACE ( 'NONE', #1995, 4.999999999999997335 ) ;
#1240=LINE ( 'NONE', #6306, #3589 ) ;
#1245=FACE_BOUND ( 'NONE', #1120, .T. ) ;
#1252=EDGE_LOOP ( 'NONE', ( #4195, #5505 ) ) ;
#1274=EDGE_CURVE ( 'NONE', #2969, #7545, #6079, .T. ) ;
#1276=EDGE_CURVE ( 'NONE', #4446, #7545, #2128, .T. ) ;
#1279=CARTESIAN_POINT ( 'NONE',  ( 0.000000000000000000, 0.000000000000000000, 0.000000000000000000 ) ) ;
#1283=CARTESIAN_POINT ( 'NONE',  ( 27.35000000000001208, -29.99999999999997868, 1.734723475976807094E-15 ) ) ;
#1293=AXIS2_PLACEMENT_3D ( 'NONE', #30, #4562, #1917 ) ;
#1304=VECTOR ( 'NONE', #5066, 1000.000000000000000 ) ;
#1316=AXIS2_PLACEMENT_3D ( 'NONE', #2410, #5655, #7606 ) ;
#1321=FACE_BOUND ( 'NONE', #4122, .T. ) ;
#1324=STYLED_ITEM ( 'NONE', ( #109 ), #6657 ) ;
#1327=PLANE ( 'NONE',  #8101 ) ;
#1335=AXIS2_PLACEMENT_3D ( 'NONE', #2275, #4809, #5967 ) ;
#1339=DIRECTION ( 'NONE',  ( 1.000000000000000000, 0.000000000000000000, 0.000000000000000000 ) ) ;
#1343=EDGE_CURVE ( 'NONE', #4949, #1038, #675, .T. ) ;
#1356=EDGE_LOOP ( 'NONE', ( #3757, #2384 ) ) ;
#1366=DIRECTION ( 'NONE',  ( 1.000000000000000000, 0.000000000000000000, 0.000000000000000000 ) ) ;
#1367=CARTESIAN_POINT ( 'NONE',  ( 0.000000000000000000, 0.000000000000000000, 0.000000000000000000 ) ) ;
#1373=ORIENTED_EDGE ( 'NONE', *, *, #7808, .T. ) ;
#1382=CARTESIAN_POINT ( 'NONE',  ( -39.99999999999999289, -39.99999999999999289, 10.00000000000000000 ) ) ;
#1385=ORIENTED_EDGE ( 'NONE', *, *, #1137, .F. ) ;
#1394=ORIENTED_EDGE ( 'NONE', *, *, #4048, .T. ) ;
#1402=EDGE_CURVE ( 'NONE', #2014, #5401, #5202, .T. ) ;
#1403=FACE_OUTER_BOUND ( 'NONE', #1036, .T. ) ;
#1420=EDGE_CURVE ( 'NONE', #5767, #4437, #7892, .T. ) ;
#1431=CARTESIAN_POINT ( 'NONE',  ( 29.99999999999997868, 30.00000000000001421, 10.00000000000000000 ) ) ;
#1440=( NAMED_UNIT ( * ) SI_UNIT ( $, .STERADIAN. ) SOLID_ANGLE_UNIT ( ) );
#1449=AXIS2_PLACEMENT_3D ( 'NONE', #678, #2598, #5589 ) ;
#1450=( NAMED_UNIT ( * ) PLANE_ANGLE_UNIT ( ) SI_UNIT ( $, .RADIAN. ) );
#1452=CIRCLE ( 'NONE', #2643, 7.000000000000000000 ) ;
#1455=VECTOR ( 'NONE', #6425, 1000.000000000000000 ) ;
#1467=CIRCLE ( 'NONE', #1198, 2.650000000000010125 ) ;
#1471=VECTOR ( 'NONE', #2210, 1000.000000000000000 ) ;
#1472=EDGE_LOOP ( 'NONE', ( #4035, #5326 ) ) ;
#1484=FACE_OUTER_BOUND ( 'NONE', #4253, .T. ) ;
#1489=ADVANCED_FACE ( 'NONE', ( #4795 ), #6738, .F. ) ;
#1494=VERTEX_POINT ( 'NONE', #2996 ) ;
#1498=ORIENTED_EDGE ( 'NONE', *, *, #8120, .T. ) ;
#1506=EDGE_CURVE ( 'NONE', #3838, #1494, #5542, .T. ) ;
#1508=DIRECTION ( 'NONE',  ( -0.000000000000000000, -0.000000000000000000, 1.000000000000000000 ) ) ;
#1533=ORIENTED_EDGE ( 'NONE', *, *, #3542, .F. ) ;
#1537=LINE ( 'NONE', #7107, #5041 ) ;
#1538=PRODUCT_CONTEXT ( 'NONE', #2541, 'mechanical' ) ;
#1539=EDGE_CURVE ( 'NONE', #4465, #1812, #6983, .T. ) ;
#1540=ORIENTED_EDGE ( 'NONE', *, *, #920, .F. ) ;
#1548=DIRECTION ( 'NONE',  ( -0.000000000000000000, -0.000000000000000000, -1.000000000000000000 ) ) ;
#1573=ORIENTED_EDGE ( 'NONE', *, *, #7711, .T. ) ;
#1580=CARTESIAN_POINT ( 'NONE',  ( -29.99999999999999289, 30.00000000000000711, 10.00000000000000000 ) ) ;
#1587=AXIS2_PLACEMENT_3D ( 'NONE', #3942, #5152, #6454 ) ;
#1590=ORIENTED_EDGE ( 'NONE', *, *, #596, .F. ) ;
#1609=VERTEX_POINT ( 'NONE', #3092 ) ;
#1610=DIRECTION ( 'NONE',  ( 1.000000000000000000, 0.000000000000000000, 0.000000000000000000 ) ) ;
#1624=AXIS2_PLACEMENT_3D ( 'NONE', #1580, #2325, #7348 ) ;
#1634=EDGE_CURVE ( 'NONE', #3388, #3918, #4571, .T. ) ;
#1636=CARTESIAN_POINT ( 'NONE',  ( 30.00000000000001066, -29.99999999999997868, 4.599999999999997868 ) ) ;
#1640=ORIENTED_EDGE ( 'NONE', *, *, #3292, .F. ) ;
#1643=CARTESIAN_POINT ( 'NONE',  ( -32.64999999999999147, 30.00000000000000711, 1.734723475976807094E-15 ) ) ;
#1653=DIRECTION ( 'NONE',  ( 1.000000000000000000, 0.000000000000000000, 0.000000000000000000 ) ) ;
#1662=FACE_BOUND ( 'NONE', #5496, .T. ) ;
#1680=DIRECTION ( 'NONE',  ( 1.000000000000000000, 0.000000000000000000, 0.000000000000000000 ) ) ;
#1694=FACE_OUTER_BOUND ( 'NONE', #2539, .T. ) ;
#1703=CARTESIAN_POINT ( 'NONE',  ( -24.99999999999999289, 30.00000000000000711, 10.00000000000000000 ) ) ;
#1707=CLOSED_SHELL ( 'NONE', ( #1053, #6857, #3744, #7849, #52, #3177, #8013, #7380, #2542, #877, #4577, #6237, #6128, #1489, #7472, #6294, #5255, #4884, #6339, #7045, #4476, #401, #6557, #1004, #4173, #5121, #2135, #4084, #4825, #4518, #2590, #7192, #5543, #7520, #3570, #2344, #5990 ) ) ;
#1712=EDGE_LOOP ( 'NONE', ( #5973, #1590 ) ) ;
#1718=UNCERTAINTY_MEASURE_WITH_UNIT (LENGTH_MEASURE( 1.000000000000000082E-05 ), #4596, 'distance_accuracy_value', 'NONE');
#1719=VECTOR ( 'NONE', #4707, 1000.000000000000000 ) ;
#1739=AXIS2_PLACEMENT_3D ( 'NONE', #6960, #7592, #688 ) ;
#1745=AXIS2_PLACEMENT_3D ( 'NONE', #1367, #5806, #101 ) ;
#1751=CARTESIAN_POINT ( 'NONE',  ( 29.99999999999997868, 30.00000000000001421, 1.734723475976807094E-15 ) ) ;
#1761=ORIENTED_EDGE ( 'NONE', *, *, #6798, .F. ) ;
#1763=CARTESIAN_POINT ( 'NONE',  ( 25.00000000000001421, -29.99999999999997868, 10.00000000000000000 ) ) ;
#1778=CARTESIAN_POINT ( 'NONE',  ( -39.99999999999999289, -39.99999999999999289, 0.000000000000000000 ) ) ;
#1782=PRODUCT_DEFINITION ( 'UNKNOWN', '', #2577, #5093 ) ;
#1796=AXIS2_PLACEMENT_3D ( 'NONE', #1751, #6803, #7675 ) ;
#1809=EDGE_CURVE ( 'NONE', #583, #4585, #5397, .T. ) ;
#1811=ORIENTED_EDGE ( 'NONE', *, *, #2057, .F. ) ;
#1812=VERTEX_POINT ( 'NONE', #4186 ) ;
#1824=DIRECTION ( 'NONE',  ( -0.000000000000000000, -0.000000000000000000, -1.000000000000000000 ) ) ;
#1830=CARTESIAN_POINT ( 'NONE',  ( 35.00000000000000000, -29.99999999999997868, 10.00000000000000000 ) ) ;
#1836=ORIENTED_EDGE ( 'NONE', *, *, #7656, .F. ) ;
#1837=VECTOR ( 'NONE', #2638, 1000.000000000000000 ) ;
#1850=AXIS2_PLACEMENT_3D ( 'NONE', #1970, #4420, #2016 ) ;
#1855=VERTEX_POINT ( 'NONE', #5521 ) ;
#1859=CIRCLE ( 'NONE', #7021, 4.999999999999993783 ) ;
#1869=DIRECTION ( 'NONE',  ( 1.000000000000000000, 0.000000000000000000, 0.000000000000000000 ) ) ;
#1872=AXIS2_PLACEMENT_3D ( 'NONE', #4684, #3801, #5668 ) ;
#1885=DIRECTION ( 'NONE',  ( -0.000000000000000000, -0.000000000000000000, -1.000000000000000000 ) ) ;
#1893=DIRECTION ( 'NONE',  ( -0.000000000000000000, -0.000000000000000000, 1.000000000000000000 ) ) ;
#1899=VERTEX_POINT ( 'NONE', #3017 ) ;
#1906=AXIS2_PLACEMENT_3D ( 'NONE', #2824, #7310, #276 ) ;
#1913=FACE_OUTER_BOUND ( 'NONE', #159, .T. ) ;
#1917=DIRECTION ( 'NONE',  ( 1.000000000000000000, 0.000000000000000000, 0.000000000000000000 ) ) ;
#1927=ORIENTED_EDGE ( 'NONE', *, *, #6539, .T. ) ;
#1930=CARTESIAN_POINT ( 'NONE',  ( -30.00000000000000355, -29.99999999999999289, 10.00000000000000000 ) ) ;
#1934=VECTOR ( 'NONE', #2811, 1000.000000000000000 ) ;
#1940=EDGE_CURVE ( 'NONE', #3623, #1156, #4198, .T. ) ;
#1970=CARTESIAN_POINT ( 'NONE',  ( 0.000000000000000000, 0.000000000000000000, 3.851859888774471706E-31 ) ) ;
#1979=FACE_BOUND ( 'NONE', #7402, .T. ) ;
#1990=CYLINDRICAL_SURFACE ( 'NONE', #372, 7.000000000000000000 ) ;
#1991=CARTESIAN_POINT ( 'NONE',  ( 0.000000000000000000, 0.000000000000000000, 18.00000000000000355 ) ) ;
#1995=AXIS2_PLACEMENT_3D ( 'NONE', #27, #4943, #6795 ) ;
#1996=FACE_OUTER_BOUND ( 'NONE', #7227, .T. ) ;
#2000=CIRCLE ( 'NONE', #4383, 2.649999999999999467 ) ;
#2014=VERTEX_POINT ( 'NONE', #7638 ) ;
#2016=DIRECTION ( 'NONE',  ( -1.000000000000000000, 0.000000000000000000, 0.000000000000000000 ) ) ;
#2027=DIRECTION ( 'NONE',  ( -0.000000000000000000, -0.000000000000000000, -1.000000000000000000 ) ) ;
#2029=DIRECTION ( 'NONE',  ( -1.000000000000000000, 0.000000000000000000, 0.000000000000000000 ) ) ;
#2035=AXIS2_PLACEMENT_3D ( 'NONE', #7289, #2763, #7240 ) ;
#2046=ORIENTED_EDGE ( 'NONE', *, *, #3723, .F. ) ;
#2054=ORIENTED_EDGE ( 'NONE', *, *, #1506, .T. ) ;
#2057=EDGE_CURVE ( 'NONE', #314, #5998, #7119, .T. ) ;
#2063=FACE_BOUND ( 'NONE', #5582, .T. ) ;
#2069=LINE ( 'NONE', #809, #1934 ) ;
#2071=( LENGTH_UNIT ( ) NAMED_UNIT ( * ) SI_UNIT ( .MILLI., .METRE. ) );
#2081=ORIENTED_EDGE ( 'NONE', *, *, #4258, .T. ) ;
#2106=ORIENTED_EDGE ( 'NONE', *, *, #7727, .F. ) ;
#2110=AXIS2_PLACEMENT_3D ( 'NONE', #6934, #8169, #8134 ) ;
#2113=DIRECTION ( 'NONE',  ( -0.000000000000000000, -0.000000000000000000, 1.000000000000000000 ) ) ;
#2115=VERTEX_POINT ( 'NONE', #180 ) ;
#2116=CIRCLE ( 'NONE', #4910, 4.999999999999993783 ) ;
#2118=AXIS2_PLACEMENT_3D ( 'NONE', #5795, #6919, #7704 ) ;
#2120=ORIENTED_EDGE ( 'NONE', *, *, #621, .F. ) ;
#2124=FACE_BOUND ( 'NONE', #2902, .T. ) ;
#2128=CIRCLE ( 'NONE', #3206, 4.999999999999993783 ) ;
#2135=ADVANCED_FACE ( 'NONE', ( #2142, #1484 ), #6036, .F. ) ;
#2136=EDGE_CURVE ( 'NONE', #4874, #1609, #5617, .T. ) ;
#2140=SURFACE_STYLE_USAGE ( .BOTH. , #6033 ) ;
#2142=FACE_BOUND ( 'NONE', #8138, .T. ) ;
#2152=DIRECTION ( 'NONE',  ( 1.000000000000000000, 0.000000000000000000, -0.000000000000000000 ) ) ;
#2156=EDGE_LOOP ( 'NONE', ( #6877, #955, #1394, #7063 ) ) ;
#2159=DIRECTION ( 'NONE',  ( -0.000000000000000000, -0.000000000000000000, 1.000000000000000000 ) ) ;
#2165=ORIENTED_EDGE ( 'NONE', *, *, #4599, .T. ) ;
#2172=CARTESIAN_POINT ( 'NONE',  ( 27.34999999999998010, 30.00000000000001421, 4.599999999999997868 ) ) ;
#2175=CARTESIAN_POINT ( 'NONE',  ( 0.000000000000000000, 0.000000000000000000, 18.00000000000000355 ) ) ;
#2186=CARTESIAN_POINT ( 'NONE',  ( -30.00000000000000355, -29.99999999999999289, 10.00000000000000000 ) ) ;
#2193=ORIENTED_EDGE ( 'NONE', *, *, #3938, .T. ) ;
#2195=CYLINDRICAL_SURFACE ( 'NONE', #5562, 4.999999999999997335 ) ;
#2204=VECTOR ( 'NONE', #7910, 1000.000000000000000 ) ;
#2205=VERTEX_POINT ( 'NONE', #7898 ) ;
#2210=DIRECTION ( 'NONE',  ( -0.000000000000000000, -0.000000000000000000, 1.000000000000000000 ) ) ;
#2225=CARTESIAN_POINT ( 'NONE',  ( -34.99999999999999289, -29.99999999999999289, 10.00000000000000000 ) ) ;
#2245=DIRECTION ( 'NONE',  ( -0.000000000000000000, -0.000000000000000000, 1.000000000000000000 ) ) ;
#2249=AXIS2_PLACEMENT_3D ( 'NONE', #7649, #739, #2499 ) ;
#2253=CARTESIAN_POINT ( 'NONE',  ( -39.99999999999999289, 40.00000000000000711, 10.00000000000000000 ) ) ;
#2260=DIRECTION ( 'NONE',  ( -1.000000000000000000, 0.000000000000000000, 0.000000000000000000 ) ) ;
#2261=VECTOR ( 'NONE', #5136, 1000.000000000000000 ) ;
#2275=CARTESIAN_POINT ( 'NONE',  ( 30.00000000000001066, -29.99999999999997868, 10.00000000000000000 ) ) ;
#2278=ORIENTED_EDGE ( 'NONE', *, *, #3292, .T. ) ;
#2285=FACE_OUTER_BOUND ( 'NONE', #4077, .T. ) ;
#2295=LINE ( 'NONE', #2253, #7936 ) ;
#2298=ORIENTED_EDGE ( 'NONE', *, *, #7692, .T. ) ;
#2301=EDGE_CURVE ( 'NONE', #3918, #2562, #6164, .T. ) ;
#2304=( LENGTH_UNIT ( ) NAMED_UNIT ( * ) SI_UNIT ( .MILLI., .METRE. ) );
#2312=DIRECTION ( 'NONE',  ( 0.000000000000000000, 0.000000000000000000, 1.000000000000000000 ) ) ;
#2314=DIRECTION ( 'NONE',  ( -0.000000000000000000, -0.000000000000000000, 1.000000000000000000 ) ) ;
#2315=ORIENTED_EDGE ( 'NONE', *, *, #1097, .T. ) ;
#2317=PRODUCT ( 'base', 'base', '', ( #1538 ) ) ;
#2320=VERTEX_POINT ( 'NONE', #4977 ) ;
#2325=DIRECTION ( 'NONE',  ( -0.000000000000000000, -0.000000000000000000, 1.000000000000000000 ) ) ;
#2330=FACE_OUTER_BOUND ( 'NONE', #6430, .T. ) ;
#2344=ADVANCED_FACE ( 'NONE', ( #6297, #602 ), #3145, .F. ) ;
#2354=EDGE_CURVE ( 'NONE', #5401, #2014, #5609, .T. ) ;
#2356=EDGE_LOOP ( 'NONE', ( #7360, #5590, #430, #4551 ) ) ;
#2377=MECHANICAL_DESIGN_GEOMETRIC_PRESENTATION_REPRESENTATION('',(#1324),#3852);
#2382=DIRECTION ( 'NONE',  ( 0.000000000000000000, 0.000000000000000000, -1.000000000000000000 ) ) ;
#2384=ORIENTED_EDGE ( 'NONE', *, *, #7020, .T. ) ;
#2394=DIRECTION ( 'NONE',  ( -1.000000000000000000, -0.000000000000000000, -0.000000000000000000 ) ) ;
#2403=DIRECTION ( 'NONE',  ( -0.000000000000000000, -0.000000000000000000, 1.000000000000000000 ) ) ;
#2407=VERTEX_POINT ( 'NONE', #5395 ) ;
#2408=CARTESIAN_POINT ( 'NONE',  ( -27.35000000000000142, -29.99999999999999289, 4.599999999999997868 ) ) ;
#2410=CARTESIAN_POINT ( 'NONE',  ( 30.00000000000001066, -29.99999999999997868, 4.599999999999997868 ) ) ;
#2421=CARTESIAN_POINT ( 'NONE',  ( 30.00000000000001066, -29.99999999999997868, 4.599999999999997868 ) ) ;
#2425=VECTOR ( 'NONE', #2394, 1000.000000000000000 ) ;
#2426=EDGE_LOOP ( 'NONE', ( #5090, #7369, #8009, #4999 ) ) ;
#2434=DIRECTION ( 'NONE',  ( -0.000000000000000000, -0.000000000000000000, 1.000000000000000000 ) ) ;
#2436=ORIENTED_EDGE ( 'NONE', *, *, #4285, .T. ) ;
#2438=FACE_BOUND ( 'NONE', #6318, .T. ) ;
#2447=ORIENTED_EDGE ( 'NONE', *, *, #5049, .T. ) ;
#2450=FACE_OUTER_BOUND ( 'NONE', #7181, .T. ) ;
#2459=ORIENTED_EDGE ( 'NONE', *, *, #4862, .T. ) ;
#2470=DIRECTION ( 'NONE',  ( -1.000000000000000000, 0.000000000000000000, -0.000000000000000000 ) ) ;
#2475=SHAPE_REPRESENTATION ( 'base', ( #1587 ), #517 ) ;
#2476=ORIENTED_EDGE ( 'NONE', *, *, #8182, .F. ) ;
#2481=DIRECTION ( 'NONE',  ( -1.000000000000000000, 0.000000000000000000, -0.000000000000000000 ) ) ;
#2483=DIRECTION ( 'NONE',  ( -0.000000000000000000, -0.000000000000000000, 1.000000000000000000 ) ) ;
#2489=DIRECTION ( 'NONE',  ( 0.000000000000000000, 0.000000000000000000, 1.000000000000000000 ) ) ;
#2499=DIRECTION ( 'NONE',  ( 1.000000000000000000, 0.000000000000000000, 0.000000000000000000 ) ) ;
#2529=FACE_BOUND ( 'NONE', #7810, .T. ) ;
#2532=CIRCLE ( 'NONE', #252, 4.999999999999997335 ) ;
#2539=EDGE_LOOP ( 'NONE', ( #3915, #624, #5716, #7688 ) ) ;
#2541=APPLICATION_CONTEXT ( 'automotive_design' ) ;
#2542=ADVANCED_FACE ( 'NONE', ( #2285 ), #7966, .F. ) ;
#2549=EDGE_LOOP ( 'NONE', ( #2046, #1224, #5787, #2867 ) ) ;
#2558=VERTEX_POINT ( 'NONE', #3618 ) ;
#2562=VERTEX_POINT ( 'NONE', #4819 ) ;
#2577=PRODUCT_DEFINITION_FORMATION_WITH_SPECIFIED_SOURCE ( 'ANY', '', #2317, .NOT_KNOWN. ) ;
#2581=SURFACE_STYLE_FILL_AREA ( #768 ) ;
#2590=ADVANCED_FACE ( 'NONE', ( #7843 ), #7259, .F. ) ;
#2598=DIRECTION ( 'NONE',  ( -0.000000000000000000, -0.000000000000000000, -1.000000000000000000 ) ) ;
#2608=EDGE_CURVE ( 'NONE', #4530, #5459, #7385, .T. ) ;
#2611=DIRECTION ( 'NONE',  ( 0.000000000000000000, 0.000000000000000000, -1.000000000000000000 ) ) ;
#2616=ORIENTED_EDGE ( 'NONE', *, *, #1539, .F. ) ;
#2619=FACE_OUTER_BOUND ( 'NONE', #5236, .T. ) ;
#2625=ORIENTED_EDGE ( 'NONE', *, *, #1211, .F. ) ;
#2638=DIRECTION ( 'NONE',  ( -0.000000000000000000, -0.000000000000000000, -1.000000000000000000 ) ) ;
#2643=AXIS2_PLACEMENT_3D ( 'NONE', #2825, #536, #4952 ) ;
#2649=DIRECTION ( 'NONE',  ( -0.000000000000000000, -0.000000000000000000, -1.000000000000000000 ) ) ;
#2652=STYLED_ITEM ( 'NONE', ( #3425 ), #6832 ) ;
#2659=VECTOR ( 'NONE', #2483, 1000.000000000000000 ) ;
#2663=ORIENTED_EDGE ( 'NONE', *, *, #6259, .F. ) ;
#2671=DIRECTION ( 'NONE',  ( 0.000000000000000000, 0.000000000000000000, -1.000000000000000000 ) ) ;
#2685=CARTESIAN_POINT ( 'NONE',  ( 0.000000000000000000, 0.000000000000000000, 18.00000000000000355 ) ) ;
#2687=DIRECTION ( 'NONE',  ( -0.000000000000000000, -0.000000000000000000, 1.000000000000000000 ) ) ;
#2710=ORIENTED_EDGE ( 'NONE', *, *, #1809, .T. ) ;
#2711=ORIENTED_EDGE ( 'NONE', *, *, #5389, .T. ) ;
#2718=( NAMED_UNIT ( * ) PLANE_ANGLE_UNIT ( ) SI_UNIT ( $, .RADIAN. ) );
#2736=EDGE_CURVE ( 'NONE', #1038, #4949, #5219, .T. ) ;
#2737=CIRCLE ( 'NONE', #3150, 2.649999999999999467 ) ;
#2745=ORIENTED_EDGE ( 'NONE', *, *, #6483, .F. ) ;
#2748=DIRECTION ( 'NONE',  ( 0.000000000000000000, 0.000000000000000000, 1.000000000000000000 ) ) ;
#2759=( NAMED_UNIT ( * ) SI_UNIT ( $, .STERADIAN. ) SOLID_ANGLE_UNIT ( ) );
#2763=DIRECTION ( 'NONE',  ( 0.000000000000000000, 0.000000000000000000, 1.000000000000000000 ) ) ;
#2765=ORIENTED_EDGE ( 'NONE', *, *, #4048, .F. ) ;
#2774=DIRECTION ( 'NONE',  ( 0.000000000000000000, 0.000000000000000000, 1.000000000000000000 ) ) ;
#2811=DIRECTION ( 'NONE',  ( -0.000000000000000000, -0.000000000000000000, 1.000000000000000000 ) ) ;
#2824=CARTESIAN_POINT ( 'NONE',  ( 30.00000000000001066, -29.99999999999997868, 10.00000000000000000 ) ) ;
#2825=CARTESIAN_POINT ( 'NONE',  ( 0.000000000000000000, 0.000000000000000000, 10.00000000000000000 ) ) ;
#2835=FACE_OUTER_BOUND ( 'NONE', #5212, .T. ) ;
#2849=DIRECTION ( 'NONE',  ( -0.000000000000000000, -0.000000000000000000, 1.000000000000000000 ) ) ;
#2850=LINE ( 'NONE', #934, #1006 ) ;
#2860=CARTESIAN_POINT ( 'NONE',  ( 0.000000000000000000, 0.000000000000000000, 18.00000000000000355 ) ) ;
#2867=ORIENTED_EDGE ( 'NONE', *, *, #82, .T. ) ;
#2869=ORIENTED_EDGE ( 'NONE', *, *, #5232, .T. ) ;
#2876=EDGE_CURVE ( 'NONE', #7000, #4888, #2737, .T. ) ;
#2880=DIRECTION ( 'NONE',  ( -0.000000000000000000, -0.000000000000000000, 1.000000000000000000 ) ) ;
#2893=CARTESIAN_POINT ( 'NONE',  ( 29.99999999999997868, 30.00000000000001421, 4.599999999999997868 ) ) ;
#2895=VECTOR ( 'NONE', #219, 1000.000000000000000 ) ;
#2902=EDGE_LOOP ( 'NONE', ( #3475, #808 ) ) ;
#2911=AXIS2_PLACEMENT_3D ( 'NONE', #5224, #2748, #246 ) ;
#2922=VECTOR ( 'NONE', #514, 1000.000000000000000 ) ;
#2966=EDGE_CURVE ( 'NONE', #4874, #1855, #2850, .T. ) ;
#2969=VERTEX_POINT ( 'NONE', #264 ) ;
#2971=AXIS2_PLACEMENT_3D ( 'NONE', #4804, #4136, #1610 ) ;
#2974=DIRECTION ( 'NONE',  ( -0.000000000000000000, -0.000000000000000000, 1.000000000000000000 ) ) ;
#2983=DIRECTION ( 'NONE',  ( 1.000000000000000000, 0.000000000000000000, 0.000000000000000000 ) ) ;
#2990=DIRECTION ( 'NONE',  ( -1.000000000000000000, -0.000000000000000000, -0.000000000000000000 ) ) ;
#2996=CARTESIAN_POINT ( 'NONE',  ( 32.64999999999997726, 30.00000000000001421, 4.599999999999997868 ) ) ;
#2998=ORIENTED_EDGE ( 'NONE', *, *, #6498, .T. ) ;
#3017=CARTESIAN_POINT ( 'NONE',  ( 35.00000000000000000, -29.99999999999997868, 4.599999999999997868 ) ) ;
#3018=ORIENTED_EDGE ( 'NONE', *, *, #1137, .T. ) ;
#3022=DIRECTION ( 'NONE',  ( 0.000000000000000000, 0.000000000000000000, -1.000000000000000000 ) ) ;
#3039=CARTESIAN_POINT ( 'NONE',  ( -39.99999999999999289, 40.00000000000000711, 10.00000000000000000 ) ) ;
#3075=CARTESIAN_POINT ( 'NONE',  ( -39.99999999999999289, 40.00000000000000711, 10.00000000000000000 ) ) ;
#3088=CYLINDRICAL_SURFACE ( 'NONE', #1449, 2.650000000000003020 ) ;
#3092=CARTESIAN_POINT ( 'NONE',  ( 10.00000000000000000, 1.224646799147353256E-15, 18.00000000000000355 ) ) ;
#3106=EDGE_CURVE ( 'NONE', #1609, #6979, #5013, .T. ) ;
#3109=DIRECTION ( 'NONE',  ( -0.000000000000000000, -0.000000000000000000, 1.000000000000000000 ) ) ;
#3125=CARTESIAN_POINT ( 'NONE',  ( 2.650000000000003020, 3.245314017740489906E-16, 0.000000000000000000 ) ) ;
#3127=EDGE_CURVE ( 'NONE', #3432, #5625, #7536, .T. ) ;
#3132=CARTESIAN_POINT ( 'NONE',  ( -39.99999999999999289, -39.99999999999999289, 0.000000000000000000 ) ) ;
#3141=DIRECTION ( 'NONE',  ( 1.000000000000000000, 0.000000000000000000, 0.000000000000000000 ) ) ;
#3145=PLANE ( 'NONE',  #3353 ) ;
#3148=EDGE_LOOP ( 'NONE', ( #6232, #4727, #272, #1100 ) ) ;
#3150=AXIS2_PLACEMENT_3D ( 'NONE', #3210, #3909, #699 ) ;
#3153=PLANE ( 'NONE',  #5940 ) ;
#3155=DIRECTION ( 'NONE',  ( -1.000000000000000000, 0.000000000000000000, 0.000000000000000000 ) ) ;
#3174=CARTESIAN_POINT ( 'NONE',  ( 24.99999999999998224, 30.00000000000001421, 4.599999999999997868 ) ) ;
#3177=ADVANCED_FACE ( 'NONE', ( #6997 ), #6335, .F. ) ;
#3180=CIRCLE ( 'NONE', #5294, 2.649999999999995914 ) ;
#3187=AXIS2_PLACEMENT_3D ( 'NONE', #5734, #3109, #1104 ) ;
#3204=EDGE_CURVE ( 'NONE', #4768, #3881, #7533, .T. ) ;
#3206=AXIS2_PLACEMENT_3D ( 'NONE', #469, #6746, #6125 ) ;
#3209=CYLINDRICAL_SURFACE ( 'NONE', #6080, 2.649999999999995914 ) ;
#3210=CARTESIAN_POINT ( 'NONE',  ( -29.99999999999999289, 30.00000000000000711, 4.599999999999997868 ) ) ;
#3238=DIRECTION ( 'NONE',  ( 1.000000000000000000, 0.000000000000000000, 0.000000000000000000 ) ) ;
#3253=ORIENTED_EDGE ( 'NONE', *, *, #1634, .T. ) ;
#3255=CARTESIAN_POINT ( 'NONE',  ( -4.999999999999993783, 0.000000000000000000, 5.400000000000002132 ) ) ;
#3260=ORIENTED_EDGE ( 'NONE', *, *, #7203, .T. ) ;
#3269=CARTESIAN_POINT ( 'NONE',  ( 2.650000000000003020, 3.245314017740489906E-16, 10.00000000000000000 ) ) ;
#3271=CARTESIAN_POINT ( 'NONE',  ( -34.99999999999999289, 30.00000000000000711, 10.00000000000000000 ) ) ;
#3281=CARTESIAN_POINT ( 'NONE',  ( 0.000000000000000000, 0.000000000000000000, 0.000000000000000000 ) ) ;
#3290=CARTESIAN_POINT ( 'NONE',  ( 32.64999999999997726, 30.00000000000001421, 1.734723475976807094E-15 ) ) ;
#3292=EDGE_CURVE ( 'NONE', #8100, #3918, #6492, .T. ) ;
#3296=VERTEX_POINT ( 'NONE', #4046 ) ;
#3310=CIRCLE ( 'NONE', #3187, 4.999999999999997335 ) ;
#3312=DIRECTION ( 'NONE',  ( 1.000000000000000000, 0.000000000000000000, 0.000000000000000000 ) ) ;
#3318=CIRCLE ( 'NONE', #2118, 2.650000000000003020 ) ;
#3319=FACE_OUTER_BOUND ( 'NONE', #506, .T. ) ;
#3333=AXIS2_PLACEMENT_3D ( 'NONE', #6627, #2312, #393 ) ;
#3341=ORIENTED_EDGE ( 'NONE', *, *, #5153, .F. ) ;
#3351=CARTESIAN_POINT ( 'NONE',  ( -7.000000000000000000, 0.000000000000000000, 18.00000000000000355 ) ) ;
#3353=AXIS2_PLACEMENT_3D ( 'NONE', #5681, #2774, #2152 ) ;
#3363=DIRECTION ( 'NONE',  ( -1.000000000000000000, 0.000000000000000000, 0.000000000000000000 ) ) ;
#3380=CARTESIAN_POINT ( 'NONE',  ( 0.000000000000000000, 0.000000000000000000, 5.400000000000002132 ) ) ;
#3388=VERTEX_POINT ( 'NONE', #4252 ) ;
#3394=CARTESIAN_POINT ( 'NONE',  ( 0.000000000000000000, 0.000000000000000000, 10.00000000000000000 ) ) ;
#3402=DIRECTION ( 'NONE',  ( -0.000000000000000000, -0.000000000000000000, 1.000000000000000000 ) ) ;
#3422=AXIS2_PLACEMENT_3D ( 'NONE', #5619, #5856, #154 ) ;
#3425=PRESENTATION_STYLE_ASSIGNMENT (( #2140 ) ) ;
#3431=CIRCLE ( 'NONE', #763, 2.649999999999995914 ) ;
#3432=VERTEX_POINT ( 'NONE', #1041 ) ;
#3439=FACE_OUTER_BOUND ( 'NONE', #5969, .T. ) ;
#3469=CARTESIAN_POINT ( 'NONE',  ( -30.00000000000000355, -29.99999999999999289, 10.00000000000000000 ) ) ;
#3471=DIRECTION ( 'NONE',  ( -1.000000000000000000, 0.000000000000000000, -0.000000000000000000 ) ) ;
#3474=ORIENTED_EDGE ( 'NONE', *, *, #7782, .F. ) ;
#3475=ORIENTED_EDGE ( 'NONE', *, *, #6818, .F. ) ;
#3489=DIRECTION ( 'NONE',  ( 1.000000000000000000, 0.000000000000000000, 0.000000000000000000 ) ) ;
#3490=PLANE ( 'NONE',  #510 ) ;
#3492=CARTESIAN_POINT ( 'NONE',  ( -25.00000000000000711, -29.99999999999999289, 10.00000000000000000 ) ) ;
#3510=LINE ( 'NONE', #3351, #4259 ) ;
#3517=DIRECTION ( 'NONE',  ( -0.000000000000000000, -0.000000000000000000, -1.000000000000000000 ) ) ;
#3519=CYLINDRICAL_SURFACE ( 'NONE', #5828, 2.649999999999995914 ) ;
#3522=ORIENTED_EDGE ( 'NONE', *, *, #3974, .T. ) ;
#3526=DIRECTION ( 'NONE',  ( -0.000000000000000000, -0.000000000000000000, 1.000000000000000000 ) ) ;
#3533=ORIENTED_EDGE ( 'NONE', *, *, #968, .F. ) ;
#3542=EDGE_CURVE ( 'NONE', #6538, #3388, #3762, .T. ) ;
#3561=VECTOR ( 'NONE', #1194, 1000.000000000000000 ) ;
#3570=ADVANCED_FACE ( 'NONE', ( #46 ), #3088, .F. ) ;
#3589=VECTOR ( 'NONE', #607, 1000.000000000000000 ) ;
#3598=DIRECTION ( 'NONE',  ( -0.000000000000000000, -0.000000000000000000, 1.000000000000000000 ) ) ;
#3618=CARTESIAN_POINT ( 'NONE',  ( -34.99999999999999289, -29.99999999999999289, 10.00000000000000000 ) ) ;
#3621=LINE ( 'NONE', #7884, #642 ) ;
#3623=VERTEX_POINT ( 'NONE', #3713 ) ;
#3624=EDGE_LOOP ( 'NONE', ( #5870, #1234, #3341, #2278 ) ) ;
#3643=DIRECTION ( 'NONE',  ( -0.000000000000000000, -0.000000000000000000, -1.000000000000000000 ) ) ;
#3653=VERTEX_POINT ( 'NONE', #1167 ) ;
#3656=LINE ( 'NONE', #3075, #7932 ) ;
#3676=DIRECTION ( 'NONE',  ( 1.000000000000000000, 0.000000000000000000, 0.000000000000000000 ) ) ;
#3682=LINE ( 'NONE', #1778, #3561 ) ;
#3696=EDGE_CURVE ( 'NONE', #708, #2320, #5755, .T. ) ;
#3701=ORIENTED_EDGE ( 'NONE', *, *, #6498, .F. ) ;
#3713=CARTESIAN_POINT ( 'NONE',  ( 4.999999999999993783, 6.123233995736758394E-16, 3.851859888774471706E-31 ) ) ;
#3723=EDGE_CURVE ( 'NONE', #4768, #7000, #1537, .T. ) ;
#3728=CARTESIAN_POINT ( 'NONE',  ( -29.99999999999999289, 30.00000000000000711, 10.00000000000000000 ) ) ;
#3744=ADVANCED_FACE ( 'NONE', ( #3923 ), #788, .F. ) ;
#3757=ORIENTED_EDGE ( 'NONE', *, *, #8049, .T. ) ;
#3758=VECTOR ( 'NONE', #2159, 1000.000000000000000 ) ;
#3762=LINE ( 'NONE', #3132, #133 ) ;
#3773=CARTESIAN_POINT ( 'NONE',  ( -29.99999999999999289, 30.00000000000000711, 10.00000000000000000 ) ) ;
#3783=LINE ( 'NONE', #4402, #7162 ) ;
#3790=DIRECTION ( 'NONE',  ( -0.000000000000000000, -0.000000000000000000, 1.000000000000000000 ) ) ;
#3797=ORIENTED_EDGE ( 'NONE', *, *, #7727, .T. ) ;
#3801=DIRECTION ( 'NONE',  ( -0.000000000000000000, -0.000000000000000000, 1.000000000000000000 ) ) ;
#3829=CARTESIAN_POINT ( 'NONE',  ( 35.00000000000000000, -29.99999999999997868, 10.00000000000000000 ) ) ;
#3838=VERTEX_POINT ( 'NONE', #3290 ) ;
#3844=DIRECTION ( 'NONE',  ( 1.000000000000000000, 0.000000000000000000, 0.000000000000000000 ) ) ;
#3847=AXIS2_PLACEMENT_3D ( 'NONE', #484, #2489, #5034 ) ;
#3852=( GEOMETRIC_REPRESENTATION_CONTEXT ( 3 ) GLOBAL_UNCERTAINTY_ASSIGNED_CONTEXT ( ( #169 ) ) GLOBAL_UNIT_ASSIGNED_CONTEXT ( ( #2071, #1450, #3991 ) ) REPRESENTATION_CONTEXT ( 'NONE', 'WORKASPACE' ) );
#3856=CARTESIAN_POINT ( 'NONE',  ( -29.99999999999999289, 30.00000000000000711, 1.734723475976807094E-15 ) ) ;
#3859=VECTOR ( 'NONE', #6199, 1000.000000000000000 ) ;
#3868=DIRECTION ( 'NONE',  ( -1.000000000000000000, 0.000000000000000000, -0.000000000000000000 ) ) ;
#3880=ORIENTED_EDGE ( 'NONE', *, *, #3696, .F. ) ;
#3881=VERTEX_POINT ( 'NONE', #6059 ) ;
#3897=EDGE_CURVE ( 'NONE', #1038, #3653, #6641, .T. ) ;
#3905=ORIENTED_EDGE ( 'NONE', *, *, #6208, .T. ) ;
#3909=DIRECTION ( 'NONE',  ( -0.000000000000000000, -0.000000000000000000, 1.000000000000000000 ) ) ;
#3915=ORIENTED_EDGE ( 'NONE', *, *, #2736, .F. ) ;
#3918=VERTEX_POINT ( 'NONE', #6683 ) ;
#3923=FACE_OUTER_BOUND ( 'NONE', #6027, .T. ) ;
#3928=ORIENTED_EDGE ( 'NONE', *, *, #2057, .T. ) ;
#3938=EDGE_CURVE ( 'NONE', #2320, #3388, #3621, .T. ) ;
#3939=CARTESIAN_POINT ( 'NONE',  ( -27.34999999999999076, 30.00000000000000711, 4.599999999999997868 ) ) ;
#3942=CARTESIAN_POINT ( 'NONE',  ( 0.000000000000000000, 0.000000000000000000, 0.000000000000000000 ) ) ;
#3943=DIRECTION ( 'NONE',  ( 0.000000000000000000, 0.000000000000000000, -1.000000000000000000 ) ) ;
#3951=FACE_OUTER_BOUND ( 'NONE', #671, .T. ) ;
#3957=ORIENTED_EDGE ( 'NONE', *, *, #7710, .F. ) ;
#3961=AXIS2_PLACEMENT_3D ( 'NONE', #3773, #7626, #598 ) ;
#3974=EDGE_CURVE ( 'NONE', #1812, #3296, #1154, .T. ) ;
#3990=AXIS2_PLACEMENT_3D ( 'NONE', #6435, #2113, #5857 ) ;
#3991=( NAMED_UNIT ( * ) SI_UNIT ( $, .STERADIAN. ) SOLID_ANGLE_UNIT ( ) );
#4010=ORIENTED_EDGE ( 'NONE', *, *, #5389, .F. ) ;
#4022=CARTESIAN_POINT ( 'NONE',  ( 0.000000000000000000, 0.000000000000000000, 5.400000000000002132 ) ) ;
#4035=ORIENTED_EDGE ( 'NONE', *, *, #2354, .T. ) ;
#4039=DIRECTION ( 'NONE',  ( -0.000000000000000000, -0.000000000000000000, 1.000000000000000000 ) ) ;
#4046=CARTESIAN_POINT ( 'NONE',  ( -2.650000000000010125, 0.000000000000000000, 5.400000000000002132 ) ) ;
#4048=EDGE_CURVE ( 'NONE', #6979, #1855, #4744, .T. ) ;
#4073=DIRECTION ( 'NONE',  ( -0.000000000000000000, -0.000000000000000000, 1.000000000000000000 ) ) ;
#4077=EDGE_LOOP ( 'NONE', ( #5334, #7381, #7009, #4454 ) ) ;
#4078=ORIENTED_EDGE ( 'NONE', *, *, #1809, .F. ) ;
#4084=ADVANCED_FACE ( 'NONE', ( #3951 ), #7644, .F. ) ;
#4088=FACE_OUTER_BOUND ( 'NONE', #2426, .T. ) ;
#4120=CIRCLE ( 'NONE', #3333, 7.000000000000000000 ) ;
#4122=EDGE_LOOP ( 'NONE', ( #6830, #3905 ) ) ;
#4136=DIRECTION ( 'NONE',  ( -0.000000000000000000, -0.000000000000000000, 1.000000000000000000 ) ) ;
#4137=DIRECTION ( 'NONE',  ( 1.000000000000000000, 0.000000000000000000, 0.000000000000000000 ) ) ;
#4152=DIRECTION ( 'NONE',  ( 1.000000000000000000, 0.000000000000000000, 0.000000000000000000 ) ) ;
#4159=ORIENTED_EDGE ( 'NONE', *, *, #968, .T. ) ;
#4161=ORIENTED_EDGE ( 'NONE', *, *, #5232, .F. ) ;
#4163=DIRECTION ( 'NONE',  ( -0.000000000000000000, -0.000000000000000000, 1.000000000000000000 ) ) ;
#4166=ORIENTED_EDGE ( 'NONE', *, *, #2876, .F. ) ;
#4167=DIRECTION ( 'NONE',  ( -0.000000000000000000, -0.000000000000000000, 1.000000000000000000 ) ) ;
#4169=LINE ( 'NONE', #1052, #238 ) ;
#4171=CIRCLE ( 'NONE', #1796, 2.649999999999999467 ) ;
#4173=ADVANCED_FACE ( 'NONE', ( #267 ), #4183, .F. ) ;
#4178=ORIENTED_EDGE ( 'NONE', *, *, #1539, .T. ) ;
#4183=CYLINDRICAL_SURFACE ( 'NONE', #1335, 4.999999999999993783 ) ;
#4186=CARTESIAN_POINT ( 'NONE',  ( -2.650000000000003020, 0.000000000000000000, 10.00000000000000000 ) ) ;
#4195=ORIENTED_EDGE ( 'NONE', *, *, #1276, .F. ) ;
#4198=CIRCLE ( 'NONE', #6990, 4.999999999999993783 ) ;
#4205=ORIENTED_EDGE ( 'NONE', *, *, #4599, .F. ) ;
#4207=ORIENTED_EDGE ( 'NONE', *, *, #3542, .T. ) ;
#4211=FILL_AREA_STYLE_COLOUR ( '', #6225 ) ;
#4235=VECTOR ( 'NONE', #6755, 1000.000000000000000 ) ;
#4252=CARTESIAN_POINT ( 'NONE',  ( 40.00000000000000711, -39.99999999999999289, 0.000000000000000000 ) ) ;
#4253=EDGE_LOOP ( 'NONE', ( #6174, #563 ) ) ;
#4256=EDGE_LOOP ( 'NONE', ( #4967, #5931 ) ) ;
#4258=EDGE_CURVE ( 'NONE', #4949, #402, #6215, .T. ) ;
#4259=VECTOR ( 'NONE', #6661, 1000.000000000000000 ) ;
#4285=EDGE_CURVE ( 'NONE', #5401, #1156, #3783, .T. ) ;
#4303=EDGE_CURVE ( 'NONE', #2014, #3623, #1240, .T. ) ;
#4321=EDGE_CURVE ( 'NONE', #3296, #4618, #1467, .T. ) ;
#4328=DIRECTION ( 'NONE',  ( 1.000000000000000000, 0.000000000000000000, 0.000000000000000000 ) ) ;
#4353=VECTOR ( 'NONE', #1885, 1000.000000000000000 ) ;
#4354=EDGE_LOOP ( 'NONE', ( #1573, #1173, #5720, #330 ) ) ;
#4357=CYLINDRICAL_SURFACE ( 'NONE', #1177, 7.000000000000000000 ) ;
#4358=CARTESIAN_POINT ( 'NONE',  ( 30.00000000000001066, -29.99999999999997868, 10.00000000000000000 ) ) ;
#4378=AXIS2_PLACEMENT_3D ( 'NONE', #3728, #5470, #3676 ) ;
#4383=AXIS2_PLACEMENT_3D ( 'NONE', #477, #2403, #4945 ) ;
#4396=AXIS2_PLACEMENT_3D ( 'NONE', #4638, #2880, #5383 ) ;
#4397=ORIENTED_EDGE ( 'NONE', *, *, #2354, .F. ) ;
#4402=CARTESIAN_POINT ( 'NONE',  ( -4.999999999999993783, 0.000000000000000000, 0.000000000000000000 ) ) ;
#4411=ORIENTED_EDGE ( 'NONE', *, *, #1506, .F. ) ;
#4420=DIRECTION ( 'NONE',  ( -0.000000000000000000, -0.000000000000000000, -1.000000000000000000 ) ) ;
#4437=VERTEX_POINT ( 'NONE', #4558 ) ;
#4438=FACE_OUTER_BOUND ( 'NONE', #8111, .T. ) ;
#4443=FACE_BOUND ( 'NONE', #490, .T. ) ;
#4446=VERTEX_POINT ( 'NONE', #1830 ) ;
#4447=LINE ( 'NONE', #3829, #6023 ) ;
#4454=ORIENTED_EDGE ( 'NONE', *, *, #404, .F. ) ;
#4465=VERTEX_POINT ( 'NONE', #3269 ) ;
#4468=CARTESIAN_POINT ( 'NONE',  ( -25.00000000000000711, -29.99999999999999289, 10.00000000000000000 ) ) ;
#4476=ADVANCED_FACE ( 'NONE', ( #1403 ), #4357, .F. ) ;
#4479=LINE ( 'NONE', #6500, #1455 ) ;
#4481=EDGE_CURVE ( 'NONE', #590, #2562, #3656, .T. ) ;
#4484=ORIENTED_EDGE ( 'NONE', *, *, #2736, .T. ) ;
#4485=CARTESIAN_POINT ( 'NONE',  ( 32.65000000000000568, -29.99999999999997868, 4.599999999999997868 ) ) ;
#4491=ORIENTED_EDGE ( 'NONE', *, *, #1634, .F. ) ;
#4513=DIRECTION ( 'NONE',  ( 0.000000000000000000, 0.000000000000000000, -1.000000000000000000 ) ) ;
#4518=ADVANCED_FACE ( 'NONE', ( #2063, #4593 ), #6844, .F. ) ;
#4519=CIRCLE ( 'NONE', #525, 4.999999999999993783 ) ;
#4521=CARTESIAN_POINT ( 'NONE',  ( -24.99999999999999289, 30.00000000000000711, 4.599999999999997868 ) ) ;
#4526=CARTESIAN_POINT ( 'NONE',  ( 29.99999999999997868, 30.00000000000001421, 10.00000000000000000 ) ) ;
#4527=EDGE_CURVE ( 'NONE', #7545, #4446, #1859, .T. ) ;
#4530=VERTEX_POINT ( 'NONE', #4521 ) ;
#4534=LINE ( 'NONE', #6463, #2895 ) ;
#4544=CARTESIAN_POINT ( 'NONE',  ( -30.00000000000000355, -29.99999999999999289, 4.599999999999997868 ) ) ;
#4548=ORIENTED_EDGE ( 'NONE', *, *, #6208, .F. ) ;
#4551=ORIENTED_EDGE ( 'NONE', *, *, #621, .T. ) ;
#4558=CARTESIAN_POINT ( 'NONE',  ( -32.64999999999999858, -29.99999999999999289, 4.599999999999997868 ) ) ;
#4559=CARTESIAN_POINT ( 'NONE',  ( 10.00000000000000000, 1.224646799147353256E-15, 10.00000000000000000 ) ) ;
#4562=DIRECTION ( 'NONE',  ( -0.000000000000000000, -0.000000000000000000, 1.000000000000000000 ) ) ;
#4563=VERTEX_POINT ( 'NONE', #8168 ) ;
#4571=LINE ( 'NONE', #6861, #6451 ) ;
#4577=ADVANCED_FACE ( 'NONE', ( #2450 ), #1990, .F. ) ;
#4585=VERTEX_POINT ( 'NONE', #2172 ) ;
#4589=CARTESIAN_POINT ( 'NONE',  ( 40.00000000000000711, 40.00000000000000711, 10.00000000000000000 ) ) ;
#4591=DIRECTION ( 'NONE',  ( -1.000000000000000000, 0.000000000000000000, 0.000000000000000000 ) ) ;
#4593=FACE_OUTER_BOUND ( 'NONE', #1356, .T. ) ;
#4594=CYLINDRICAL_SURFACE ( 'NONE', #6093, 10.00000000000000000 ) ;
#4596=( LENGTH_UNIT ( ) NAMED_UNIT ( * ) SI_UNIT ( .MILLI., .METRE. ) );
#4599=EDGE_CURVE ( 'NONE', #2407, #5094, #7198, .T. ) ;
#4618=VERTEX_POINT ( 'NONE', #332 ) ;
#4620=EDGE_LOOP ( 'NONE', ( #2298, #7340 ) ) ;
#4630=CIRCLE ( 'NONE', #6606, 2.649999999999999467 ) ;
#4637=AXIS2_PLACEMENT_3D ( 'NONE', #1431, #7813, #5335 ) ;
#4638=CARTESIAN_POINT ( 'NONE',  ( -29.99999999999999289, 30.00000000000000711, 10.00000000000000000 ) ) ;
#4639=AXIS2_PLACEMENT_3D ( 'NONE', #690, #143, #97 ) ;
#4654=ORIENTED_EDGE ( 'NONE', *, *, #3204, .F. ) ;
#4657=PLANE ( 'NONE',  #232 ) ;
#4669=ORIENTED_EDGE ( 'NONE', *, *, #3723, .T. ) ;
#4675=( NAMED_UNIT ( * ) PLANE_ANGLE_UNIT ( ) SI_UNIT ( $, .RADIAN. ) );
#4684=CARTESIAN_POINT ( 'NONE',  ( 29.99999999999997868, 30.00000000000001421, 4.599999999999997868 ) ) ;
#4707=DIRECTION ( 'NONE',  ( -0.000000000000000000, -0.000000000000000000, -1.000000000000000000 ) ) ;
#4709=DIRECTION ( 'NONE',  ( 0.000000000000000000, 0.000000000000000000, 1.000000000000000000 ) ) ;
#4712=ORIENTED_EDGE ( 'NONE', *, *, #6798, .T. ) ;
#4727=ORIENTED_EDGE ( 'NONE', *, *, #6571, .F. ) ;
#4737=EDGE_LOOP ( 'NONE', ( #519, #3797, #6690, #5629 ) ) ;
#4742=CIRCLE ( 'NONE', #5935, 2.649999999999999467 ) ;
#4744=CIRCLE ( 'NONE', #1165, 10.00000000000000000 ) ;
#4750=DIRECTION ( 'NONE',  ( -0.000000000000000000, -0.000000000000000000, -1.000000000000000000 ) ) ;
#4751=EDGE_CURVE ( 'NONE', #590, #708, #4169, .T. ) ;
#4752=CIRCLE ( 'NONE', #1316, 4.999999999999993783 ) ;
#4763=CIRCLE ( 'NONE', #1186, 2.649999999999995914 ) ;
#4768=VERTEX_POINT ( 'NONE', #1643 ) ;
#4784=AXIS2_PLACEMENT_3D ( 'NONE', #4544, #7069, #6442 ) ;
#4795=FACE_OUTER_BOUND ( 'NONE', #7403, .T. ) ;
#4802=EDGE_LOOP ( 'NONE', ( #453, #2476, #6388, #6100 ) ) ;
#4804=CARTESIAN_POINT ( 'NONE',  ( -29.99999999999999289, 30.00000000000000711, 10.00000000000000000 ) ) ;
#4809=DIRECTION ( 'NONE',  ( -0.000000000000000000, -0.000000000000000000, 1.000000000000000000 ) ) ;
#4819=CARTESIAN_POINT ( 'NONE',  ( -39.99999999999999289, 40.00000000000000711, 0.000000000000000000 ) ) ;
#4825=ADVANCED_FACE ( 'NONE', ( #5547 ), #379, .F. ) ;
#4828=EDGE_CURVE ( 'NONE', #3881, #4888, #6743, .T. ) ;
#4836=EDGE_LOOP ( 'NONE', ( #4078, #8179, #2054, #5631 ) ) ;
#4851=CARTESIAN_POINT ( 'NONE',  ( 34.99999999999997868, 30.00000000000001421, 4.599999999999997868 ) ) ;
#4862=EDGE_CURVE ( 'NONE', #1812, #4465, #3318, .T. ) ;
#4871=FACE_OUTER_BOUND ( 'NONE', #3624, .T. ) ;
#4874=VERTEX_POINT ( 'NONE', #18 ) ;
#4884=ADVANCED_FACE ( 'NONE', ( #749, #5722, #1979, #7589, #595, #6381 ), #7660, .F. ) ;
#4888=VERTEX_POINT ( 'NONE', #7040 ) ;
#4893=DIRECTION ( 'NONE',  ( -0.000000000000000000, -0.000000000000000000, -1.000000000000000000 ) ) ;
#4901=COLOUR_RGB ( '', 0.09019608, 0.27058824, 0.51372549) ;
#4910=AXIS2_PLACEMENT_3D ( 'NONE', #1930, #5784, #707 ) ;
#4919=DIRECTION ( 'NONE',  ( 0.000000000000000000, -0.000000000000000000, 1.000000000000000000 ) ) ;
#4921=VECTOR ( 'NONE', #1893, 1000.000000000000000 ) ;
#4943=DIRECTION ( 'NONE',  ( -0.000000000000000000, -0.000000000000000000, 1.000000000000000000 ) ) ;
#4945=DIRECTION ( 'NONE',  ( 1.000000000000000000, 0.000000000000000000, 0.000000000000000000 ) ) ;
#4949=VERTEX_POINT ( 'NONE', #719 ) ;
#4952=DIRECTION ( 'NONE',  ( 1.000000000000000000, 0.000000000000000000, 0.000000000000000000 ) ) ;
#4956=CARTESIAN_POINT ( 'NONE',  ( -2.650000000000003020, 0.000000000000000000, 0.000000000000000000 ) ) ;
#4966=( GEOMETRIC_REPRESENTATION_CONTEXT ( 3 ) GLOBAL_UNCERTAINTY_ASSIGNED_CONTEXT ( ( #5540 ) ) GLOBAL_UNIT_ASSIGNED_CONTEXT ( ( #2304, #4675, #2759 ) ) REPRESENTATION_CONTEXT ( 'NONE', 'WORKASPACE' ) );
#4967=ORIENTED_EDGE ( 'NONE', *, *, #6422, .T. ) ;
#4970=ORIENTED_EDGE ( 'NONE', *, *, #2136, .F. ) ;
#4973=CARTESIAN_POINT ( 'NONE',  ( -30.00000000000000355, -29.99999999999999289, 10.00000000000000000 ) ) ;
#4977=CARTESIAN_POINT ( 'NONE',  ( 40.00000000000000711, -39.99999999999999289, 10.00000000000000000 ) ) ;
#4983=FACE_BOUND ( 'NONE', #7567, .T. ) ;
#4999=ORIENTED_EDGE ( 'NONE', *, *, #6818, .T. ) ;
#5003=DIRECTION ( 'NONE',  ( 1.000000000000000000, 0.000000000000000000, 0.000000000000000000 ) ) ;
#5005=DIRECTION ( 'NONE',  ( 1.000000000000000000, 0.000000000000000000, 0.000000000000000000 ) ) ;
#5013=LINE ( 'NONE', #6252, #1837 ) ;
#5026=AXIS2_PLACEMENT_3D ( 'NONE', #3856, #5724, #3141 ) ;
#5029=AXIS2_PLACEMENT_3D ( 'NONE', #6624, #7244, #6087 ) ;
#5032=CARTESIAN_POINT ( 'NONE',  ( 0.000000000000000000, 0.000000000000000000, 10.00000000000000000 ) ) ;
#5034=DIRECTION ( 'NONE',  ( 1.000000000000000000, 0.000000000000000000, 0.000000000000000000 ) ) ;
#5041=VECTOR ( 'NONE', #4039, 1000.000000000000000 ) ;
#5049=EDGE_CURVE ( 'NONE', #1609, #4874, #7279, .T. ) ;
#5060=ORIENTED_EDGE ( 'NONE', *, *, #1072, .T. ) ;
#5066=DIRECTION ( 'NONE',  ( -0.000000000000000000, -0.000000000000000000, 1.000000000000000000 ) ) ;
#5090=ORIENTED_EDGE ( 'NONE', *, *, #1420, .F. ) ;
#5093=PRODUCT_DEFINITION_CONTEXT ( 'detailed design', #767, 'design' ) ;
#5094=VERTEX_POINT ( 'NONE', #7229 ) ;
#5116=CIRCLE ( 'NONE', #7206, 2.649999999999999467 ) ;
#5121=ADVANCED_FACE ( 'NONE', ( #137 ), #7114, .F. ) ;
#5136=DIRECTION ( 'NONE',  ( 0.000000000000000000, 1.000000000000000000, 0.000000000000000000 ) ) ;
#5151=FACE_OUTER_BOUND ( 'NONE', #4802, .T. ) ;
#5152=DIRECTION ( 'NONE',  ( 0.000000000000000000, 0.000000000000000000, 1.000000000000000000 ) ) ;
#5153=EDGE_CURVE ( 'NONE', #8100, #590, #2295, .T. ) ;
#5168=AXIS2_PLACEMENT_3D ( 'NONE', #5646, #8125, #8160 ) ;
#5196=AXIS2_PLACEMENT_3D ( 'NONE', #5538, #7396, #5003 ) ;
#5202=CIRCLE ( 'NONE', #256, 4.999999999999993783 ) ;
#5212=EDGE_LOOP ( 'NONE', ( #5819, #2710, #6521, #4411 ) ) ;
#5216=DIRECTION ( 'NONE',  ( -1.000000000000000000, 0.000000000000000000, -0.000000000000000000 ) ) ;
#5219=CIRCLE ( 'NONE', #6400, 2.649999999999995914 ) ;
#5224=CARTESIAN_POINT ( 'NONE',  ( 0.000000000000000000, 0.000000000000000000, 18.00000000000000355 ) ) ;
#5228=AXIS2_PLACEMENT_3D ( 'NONE', #6703, #5347, #3471 ) ;
#5231=DIRECTION ( 'NONE',  ( -0.000000000000000000, -0.000000000000000000, 1.000000000000000000 ) ) ;
#5232=EDGE_CURVE ( 'NONE', #402, #3653, #4763, .T. ) ;
#5236=EDGE_LOOP ( 'NONE', ( #1090, #4397, #2436, #2711 ) ) ;
#5255=ADVANCED_FACE ( 'NONE', ( #2330 ), #6148, .F. ) ;
#5294=AXIS2_PLACEMENT_3D ( 'NONE', #7464, #5558, #1869 ) ;
#5300=EDGE_CURVE ( 'NONE', #3653, #402, #5842, .T. ) ;
#5317=LINE ( 'NONE', #6282, #2261 ) ;
#5326=ORIENTED_EDGE ( 'NONE', *, *, #1402, .T. ) ;
#5334=ORIENTED_EDGE ( 'NONE', *, *, #5836, .F. ) ;
#5335=DIRECTION ( 'NONE',  ( 1.000000000000000000, 0.000000000000000000, 0.000000000000000000 ) ) ;
#5347=DIRECTION ( 'NONE',  ( 0.000000000000000000, 0.000000000000000000, -1.000000000000000000 ) ) ;
#5354=DIRECTION ( 'NONE',  ( -1.000000000000000000, 0.000000000000000000, 0.000000000000000000 ) ) ;
#5372=VERTEX_POINT ( 'NONE', #3174 ) ;
#5373=AXIS2_PLACEMENT_3D ( 'NONE', #5032, #7640, #6310 ) ;
#5383=DIRECTION ( 'NONE',  ( 1.000000000000000000, 0.000000000000000000, 0.000000000000000000 ) ) ;
#5389=EDGE_CURVE ( 'NONE', #1156, #3623, #6472, .T. ) ;
#5395=CARTESIAN_POINT ( 'NONE',  ( 7.000000000000000000, 8.572527594031473190E-16, 18.00000000000000355 ) ) ;
#5396=ORIENTED_EDGE ( 'NONE', *, *, #271, .T. ) ;
#5397=LINE ( 'NONE', #853, #2204 ) ;
#5401=VERTEX_POINT ( 'NONE', #3255 ) ;
#5409=ORIENTED_EDGE ( 'NONE', *, *, #1402, .F. ) ;
#5428=AXIS2_PLACEMENT_3D ( 'NONE', #7050, #2687, #1366 ) ;
#5438=CIRCLE ( 'NONE', #4639, 4.999999999999997335 ) ;
#5450=DIRECTION ( 'NONE',  ( -0.000000000000000000, -0.000000000000000000, 1.000000000000000000 ) ) ;
#5453=CARTESIAN_POINT ( 'NONE',  ( 27.35000000000001208, -29.99999999999997868, 10.00000000000000000 ) ) ;
#5457=AXIS2_PLACEMENT_3D ( 'NONE', #4526, #5231, #29 ) ;
#5459=VERTEX_POINT ( 'NONE', #194 ) ;
#5460=ORIENTED_EDGE ( 'NONE', *, *, #2876, .T. ) ;
#5467=CARTESIAN_POINT ( 'NONE',  ( 32.64999999999997726, 30.00000000000001421, 10.00000000000000000 ) ) ;
#5468=ORIENTED_EDGE ( 'NONE', *, *, #7946, .T. ) ;
#5470=DIRECTION ( 'NONE',  ( -0.000000000000000000, -0.000000000000000000, 1.000000000000000000 ) ) ;
#5476=ORIENTED_EDGE ( 'NONE', *, *, #8182, .T. ) ;
#5496=EDGE_LOOP ( 'NONE', ( #5896, #2625 ) ) ;
#5498=CYLINDRICAL_SURFACE ( 'NONE', #5196, 4.999999999999993783 ) ;
#5505=ORIENTED_EDGE ( 'NONE', *, *, #4527, .F. ) ;
#5521=CARTESIAN_POINT ( 'NONE',  ( -10.00000000000000000, 0.000000000000000000, 10.00000000000000000 ) ) ;
#5527=DIRECTION ( 'NONE',  ( 1.000000000000000000, 0.000000000000000000, -0.000000000000000000 ) ) ;
#5530=DIRECTION ( 'NONE',  ( 1.000000000000000000, 0.000000000000000000, 0.000000000000000000 ) ) ;
#5537=CARTESIAN_POINT ( 'NONE',  ( -39.99999999999999289, -39.99999999999999289, 10.00000000000000000 ) ) ;
#5538=CARTESIAN_POINT ( 'NONE',  ( -30.00000000000000355, -29.99999999999999289, 10.00000000000000000 ) ) ;
#5540=UNCERTAINTY_MEASURE_WITH_UNIT (LENGTH_MEASURE( 1.000000000000000082E-05 ), #2304, 'distance_accuracy_value', 'NONE');
#5542=LINE ( 'NONE', #5467, #7652 ) ;
#5543=ADVANCED_FACE ( 'NONE', ( #2124, #5936 ), #4657, .F. ) ;
#5547=FACE_OUTER_BOUND ( 'NONE', #2549, .T. ) ;
#5558=DIRECTION ( 'NONE',  ( -0.000000000000000000, -0.000000000000000000, 1.000000000000000000 ) ) ;
#5561=CARTESIAN_POINT ( 'NONE',  ( 32.65000000000000568, -29.99999999999997868, 10.00000000000000000 ) ) ;
#5562=AXIS2_PLACEMENT_3D ( 'NONE', #7800, #3526, #316 ) ;
#5565=DIRECTION ( 'NONE',  ( -1.000000000000000000, 0.000000000000000000, 0.000000000000000000 ) ) ;
#5580=AXIS2_PLACEMENT_3D ( 'NONE', #3469, #5993, #1226 ) ;
#5582=EDGE_LOOP ( 'NONE', ( #489, #4166 ) ) ;
#5588=CIRCLE ( 'NONE', #1872, 2.649999999999999467 ) ;
#5589=DIRECTION ( 'NONE',  ( -1.000000000000000000, 0.000000000000000000, 0.000000000000000000 ) ) ;
#5590=ORIENTED_EDGE ( 'NONE', *, *, #7692, .F. ) ;
#5603=CARTESIAN_POINT ( 'NONE',  ( 0.000000000000000000, 0.000000000000000000, 0.000000000000000000 ) ) ;
#5609=CIRCLE ( 'NONE', #6405, 4.999999999999993783 ) ;
#5611=EDGE_CURVE ( 'NONE', #4563, #5767, #3431, .T. ) ;
#5617=CIRCLE ( 'NONE', #2035, 10.00000000000000000 ) ;
#5619=CARTESIAN_POINT ( 'NONE',  ( 30.00000000000001066, -29.99999999999997868, 4.599999999999997868 ) ) ;
#5624=ORIENTED_EDGE ( 'NONE', *, *, #1343, .F. ) ;
#5625=VERTEX_POINT ( 'NONE', #3492 ) ;
#5629=ORIENTED_EDGE ( 'NONE', *, *, #2608, .F. ) ;
#5631=ORIENTED_EDGE ( 'NONE', *, *, #7656, .T. ) ;
#5646=CARTESIAN_POINT ( 'NONE',  ( 0.000000000000000000, 0.000000000000000000, 18.00000000000000355 ) ) ;
#5655=DIRECTION ( 'NONE',  ( -0.000000000000000000, -0.000000000000000000, 1.000000000000000000 ) ) ;
#5659=ORIENTED_EDGE ( 'NONE', *, *, #2966, .T. ) ;
#5668=DIRECTION ( 'NONE',  ( 1.000000000000000000, 0.000000000000000000, 0.000000000000000000 ) ) ;
#5681=CARTESIAN_POINT ( 'NONE',  ( 2.650000000000010125, 0.000000000000000000, 5.400000000000002132 ) ) ;
#5685=CARTESIAN_POINT ( 'NONE',  ( 34.99999999999997868, 30.00000000000001421, 10.00000000000000000 ) ) ;
#5695=CARTESIAN_POINT ( 'NONE',  ( 30.00000000000001066, -29.99999999999997868, 1.734723475976807094E-15 ) ) ;
#5706=LINE ( 'NONE', #3125, #6370 ) ;
#5711=CARTESIAN_POINT ( 'NONE',  ( 29.99999999999997868, 30.00000000000001421, 4.599999999999997868 ) ) ;
#5716=ORIENTED_EDGE ( 'NONE', *, *, #5300, .T. ) ;
#5720=ORIENTED_EDGE ( 'NONE', *, *, #4751, .T. ) ;
#5722=FACE_BOUND ( 'NONE', #1712, .T. ) ;
#5724=DIRECTION ( 'NONE',  ( -0.000000000000000000, -0.000000000000000000, 1.000000000000000000 ) ) ;
#5734=CARTESIAN_POINT ( 'NONE',  ( -29.99999999999999289, 30.00000000000000711, 4.599999999999997868 ) ) ;
#5746=EDGE_LOOP ( 'NONE', ( #2106, #5781, #7391, #5060 ) ) ;
#5747=ORIENTED_EDGE ( 'NONE', *, *, #4321, .T. ) ;
#5755=LINE ( 'NONE', #6986, #7550 ) ;
#5767=VERTEX_POINT ( 'NONE', #6893 ) ;
#5781=ORIENTED_EDGE ( 'NONE', *, *, #8049, .F. ) ;
#5784=DIRECTION ( 'NONE',  ( -0.000000000000000000, -0.000000000000000000, 1.000000000000000000 ) ) ;
#5787=ORIENTED_EDGE ( 'NONE', *, *, #4828, .T. ) ;
#5795=CARTESIAN_POINT ( 'NONE',  ( 0.000000000000000000, 0.000000000000000000, 10.00000000000000000 ) ) ;
#5803=DIRECTION ( 'NONE',  ( -0.000000000000000000, -0.000000000000000000, -1.000000000000000000 ) ) ;
#5806=DIRECTION ( 'NONE',  ( -0.000000000000000000, -0.000000000000000000, -1.000000000000000000 ) ) ;
#5810=FILL_AREA_STYLE_COLOUR ( '', #4901 ) ;
#5819=ORIENTED_EDGE ( 'NONE', *, *, #706, .F. ) ;
#5828=AXIS2_PLACEMENT_3D ( 'NONE', #2186, #2974, #1653 ) ;
#5836=EDGE_CURVE ( 'NONE', #2969, #1899, #7923, .T. ) ;
#5842=CIRCLE ( 'NONE', #6898, 2.649999999999995914 ) ;
#5856=DIRECTION ( 'NONE',  ( -0.000000000000000000, -0.000000000000000000, 1.000000000000000000 ) ) ;
#5857=DIRECTION ( 'NONE',  ( 1.000000000000000000, 0.000000000000000000, 0.000000000000000000 ) ) ;
#5870=ORIENTED_EDGE ( 'NONE', *, *, #2301, .T. ) ;
#5896=ORIENTED_EDGE ( 'NONE', *, *, #7808, .F. ) ;
#5904=ORIENTED_EDGE ( 'NONE', *, *, #4828, .F. ) ;
#5931=ORIENTED_EDGE ( 'NONE', *, *, #3204, .T. ) ;
#5935=AXIS2_PLACEMENT_3D ( 'NONE', #6001, #2849, #4137 ) ;
#5936=FACE_OUTER_BOUND ( 'NONE', #4620, .T. ) ;
#5940=AXIS2_PLACEMENT_3D ( 'NONE', #1279, #6963, #2481 ) ;
#5953=DIRECTION ( 'NONE',  ( -1.000000000000000000, 0.000000000000000000, 0.000000000000000000 ) ) ;
#5966=DIRECTION ( 'NONE',  ( -0.000000000000000000, -0.000000000000000000, 1.000000000000000000 ) ) ;
#5967=DIRECTION ( 'NONE',  ( 1.000000000000000000, 0.000000000000000000, 0.000000000000000000 ) ) ;
#5968=DIRECTION ( 'NONE',  ( -0.000000000000000000, -0.000000000000000000, -1.000000000000000000 ) ) ;
#5969=EDGE_LOOP ( 'NONE', ( #4548, #6664, #1498, #730 ) ) ;
#5973=ORIENTED_EDGE ( 'NONE', *, *, #1072, .F. ) ;
#5974=CIRCLE ( 'NONE', #4396, 4.999999999999993783 ) ;
#5976=EDGE_CURVE ( 'NONE', #5372, #314, #4534, .T. ) ;
#5990=ADVANCED_FACE ( 'NONE', ( #2619 ), #772, .F. ) ;
#5993=DIRECTION ( 'NONE',  ( -0.000000000000000000, -0.000000000000000000, 1.000000000000000000 ) ) ;
#5998=VERTEX_POINT ( 'NONE', #6626 ) ;
#6001=CARTESIAN_POINT ( 'NONE',  ( -30.00000000000000355, -29.99999999999999289, 4.599999999999997868 ) ) ;
#6023=VECTOR ( 'NONE', #6353, 1000.000000000000000 ) ;
#6027=EDGE_LOOP ( 'NONE', ( #2745, #5468, #3260, #6440 ) ) ;
#6033=SURFACE_SIDE_STYLE ('',( #7284 ) ) ;
#6036=PLANE ( 'NONE',  #5228 ) ;
#6039=AXIS2_PLACEMENT_3D ( 'NONE', #7401, #2382, #7980 ) ;
#6040=CARTESIAN_POINT ( 'NONE',  ( -39.99999999999999289, 40.00000000000000711, 10.00000000000000000 ) ) ;
#6059=CARTESIAN_POINT ( 'NONE',  ( -27.34999999999999076, 30.00000000000000711, 1.734723475976807094E-15 ) ) ;
#6065=DIRECTION ( 'NONE',  ( -0.000000000000000000, -0.000000000000000000, 1.000000000000000000 ) ) ;
#6079=LINE ( 'NONE', #6163, #2922 ) ;
#6080=AXIS2_PLACEMENT_3D ( 'NONE', #4358, #3790, #8042 ) ;
#6082=AXIS2_PLACEMENT_3D ( 'NONE', #3939, #3022, #1150 ) ;
#6087=DIRECTION ( 'NONE',  ( 1.000000000000000000, 0.000000000000000000, 0.000000000000000000 ) ) ;
#6093=AXIS2_PLACEMENT_3D ( 'NONE', #1991, #2649, #6499 ) ;
#6095=ORIENTED_EDGE ( 'NONE', *, *, #4303, .T. ) ;
#6100=ORIENTED_EDGE ( 'NONE', *, *, #4481, .T. ) ;
#6114=ORIENTED_EDGE ( 'NONE', *, *, #3897, .F. ) ;
#6125=DIRECTION ( 'NONE',  ( 1.000000000000000000, 0.000000000000000000, 0.000000000000000000 ) ) ;
#6128=ADVANCED_FACE ( 'NONE', ( #4983, #1321, #1913, #2438, #2529, #7633 ), #3153, .T. ) ;
#6144=DIRECTION ( 'NONE',  ( -0.000000000000000000, -0.000000000000000000, -1.000000000000000000 ) ) ;
#6148=PLANE ( 'NONE',  #7940 ) ;
#6162=EDGE_CURVE ( 'NONE', #2562, #6538, #3682, .T. ) ;
#6163=CARTESIAN_POINT ( 'NONE',  ( 25.00000000000001421, -29.99999999999997868, 10.00000000000000000 ) ) ;
#6164=LINE ( 'NONE', #8073, #2425 ) ;
#6173=CARTESIAN_POINT ( 'NONE',  ( 0.000000000000000000, 0.000000000000000000, 3.851859888774471706E-31 ) ) ;
#6174=ORIENTED_EDGE ( 'NONE', *, *, #7782, .T. ) ;
#6199=DIRECTION ( 'NONE',  ( -0.000000000000000000, -0.000000000000000000, 1.000000000000000000 ) ) ;
#6208=EDGE_CURVE ( 'NONE', #5767, #4563, #3180, .T. ) ;
#6215=LINE ( 'NONE', #5561, #2659 ) ;
#6225=COLOUR_RGB ( '', 0.09019608, 0.27058824, 0.51372549) ;
#6232=ORIENTED_EDGE ( 'NONE', *, *, #1274, .F. ) ;
#6237=ADVANCED_FACE ( 'NONE', ( #605 ), #6304, .T. ) ;
#6252=CARTESIAN_POINT ( 'NONE',  ( 10.00000000000000000, 1.224646799147353256E-15, 18.00000000000000355 ) ) ;
#6259=EDGE_CURVE ( 'NONE', #792, #5998, #6834, .T. ) ;
#6269=PLANE ( 'NONE',  #5373 ) ;
#6282=CARTESIAN_POINT ( 'NONE',  ( 40.00000000000000711, -39.99999999999999289, 10.00000000000000000 ) ) ;
#6294=ADVANCED_FACE ( 'NONE', ( #5151 ), #6390, .F. ) ;
#6297=FACE_BOUND ( 'NONE', #7452, .T. ) ;
#6299=EDGE_LOOP ( 'NONE', ( #1927, #2998 ) ) ;
#6304=CYLINDRICAL_SURFACE ( 'NONE', #5168, 10.00000000000000000 ) ;
#6306=CARTESIAN_POINT ( 'NONE',  ( 4.999999999999993783, 6.123233995736758394E-16, 0.000000000000000000 ) ) ;
#6310=DIRECTION ( 'NONE',  ( -1.000000000000000000, 0.000000000000000000, -0.000000000000000000 ) ) ;
#6318=EDGE_LOOP ( 'NONE', ( #794, #4484 ) ) ;
#6335=CYLINDRICAL_SURFACE ( 'NONE', #3961, 2.649999999999999467 ) ;
#6339=ADVANCED_FACE ( 'NONE', ( #6721, #1662 ), #3490, .T. ) ;
#6345=CARTESIAN_POINT ( 'NONE',  ( 0.000000000000000000, 0.000000000000000000, 5.400000000000002132 ) ) ;
#6353=DIRECTION ( 'NONE',  ( -0.000000000000000000, -0.000000000000000000, 1.000000000000000000 ) ) ;
#6370=VECTOR ( 'NONE', #2, 1000.000000000000000 ) ;
#6381=FACE_OUTER_BOUND ( 'NONE', #4354, .T. ) ;
#6387=CIRCLE ( 'NONE', #7582, 2.650000000000010125 ) ;
#6388=ORIENTED_EDGE ( 'NONE', *, *, #4751, .F. ) ;
#6390=PLANE ( 'NONE',  #6883 ) ;
#6400=AXIS2_PLACEMENT_3D ( 'NONE', #5695, #2434, #2983 ) ;
#6401=ORIENTED_EDGE ( 'NONE', *, *, #4862, .F. ) ;
#6405=AXIS2_PLACEMENT_3D ( 'NONE', #892, #5968, #3363 ) ;
#6422=EDGE_CURVE ( 'NONE', #3881, #4768, #4630, .T. ) ;
#6425=DIRECTION ( 'NONE',  ( -0.000000000000000000, -0.000000000000000000, -1.000000000000000000 ) ) ;
#6430=EDGE_LOOP ( 'NONE', ( #4207, #7996, #3880, #5476 ) ) ;
#6435=CARTESIAN_POINT ( 'NONE',  ( 29.99999999999997868, 30.00000000000001421, 10.00000000000000000 ) ) ;
#6440=ORIENTED_EDGE ( 'NONE', *, *, #3127, .F. ) ;
#6442=DIRECTION ( 'NONE',  ( 1.000000000000000000, 0.000000000000000000, 0.000000000000000000 ) ) ;
#6443=DIRECTION ( 'NONE',  ( -0.000000000000000000, -0.000000000000000000, 1.000000000000000000 ) ) ;
#6451=VECTOR ( 'NONE', #8147, 1000.000000000000000 ) ;
#6453=CARTESIAN_POINT ( 'NONE',  ( 30.00000000000001066, -29.99999999999997868, 10.00000000000000000 ) ) ;
#6454=DIRECTION ( 'NONE',  ( 1.000000000000000000, 0.000000000000000000, 0.000000000000000000 ) ) ;
#6463=CARTESIAN_POINT ( 'NONE',  ( 24.99999999999998224, 30.00000000000001421, 10.00000000000000000 ) ) ;
#6464=DIRECTION ( 'NONE',  ( 0.000000000000000000, 0.000000000000000000, 1.000000000000000000 ) ) ;
#6472=CIRCLE ( 'NONE', #1850, 4.999999999999993783 ) ;
#6483=EDGE_CURVE ( 'NONE', #2115, #3432, #7404, .T. ) ;
#6492=LINE ( 'NONE', #4589, #7130 ) ;
#6498=EDGE_CURVE ( 'NONE', #5094, #157, #371, .T. ) ;
#6499=DIRECTION ( 'NONE',  ( -1.000000000000000000, 0.000000000000000000, 0.000000000000000000 ) ) ;
#6500=CARTESIAN_POINT ( 'NONE',  ( -39.99999999999999289, -39.99999999999999289, 10.00000000000000000 ) ) ;
#6501=CIRCLE ( 'NONE', #5428, 2.649999999999999467 ) ;
#6515=FACE_OUTER_BOUND ( 'NONE', #4737, .T. ) ;
#6518=CARTESIAN_POINT ( 'NONE',  ( -30.00000000000000355, -29.99999999999999289, 10.00000000000000000 ) ) ;
#6521=ORIENTED_EDGE ( 'NONE', *, *, #920, .T. ) ;
#6538=VERTEX_POINT ( 'NONE', #613 ) ;
#6539=EDGE_CURVE ( 'NONE', #157, #5094, #1452, .T. ) ;
#6549=CIRCLE ( 'NONE', #2971, 4.999999999999993783 ) ;
#6557=ADVANCED_FACE ( 'NONE', ( #7562 ), #3209, .F. ) ;
#6571=EDGE_CURVE ( 'NONE', #1899, #2969, #4752, .T. ) ;
#6606=AXIS2_PLACEMENT_3D ( 'NONE', #446, #5450, #4152 ) ;
#6623=AXIS2_PLACEMENT_3D ( 'NONE', #2893, #5966, #346 ) ;
#6624=CARTESIAN_POINT ( 'NONE',  ( 0.000000000000000000, 0.000000000000000000, 10.00000000000000000 ) ) ;
#6626=CARTESIAN_POINT ( 'NONE',  ( 34.99999999999997868, 30.00000000000001421, 10.00000000000000000 ) ) ;
#6627=CARTESIAN_POINT ( 'NONE',  ( 0.000000000000000000, 0.000000000000000000, 18.00000000000000355 ) ) ;
#6641=LINE ( 'NONE', #5453, #6740 ) ;
#6642=SHAPE_DEFINITION_REPRESENTATION ( #1055, #2475 ) ;
#6656=CARTESIAN_POINT ( 'NONE',  ( -32.64999999999999858, -29.99999999999999289, 10.00000000000000000 ) ) ;
#6657=MANIFOLD_SOLID_BREP ( 'CBORE for M5 Hex Socket Head Cap Screw2', #1707 ) ;
#6661=DIRECTION ( 'NONE',  ( -0.000000000000000000, -0.000000000000000000, -1.000000000000000000 ) ) ;
#6664=ORIENTED_EDGE ( 'NONE', *, *, #1420, .T. ) ;
#6683=CARTESIAN_POINT ( 'NONE',  ( 40.00000000000000711, 40.00000000000000711, 0.000000000000000000 ) ) ;
#6690=ORIENTED_EDGE ( 'NONE', *, *, #596, .T. ) ;
#6692=DIRECTION ( 'NONE',  ( 1.000000000000000000, 0.000000000000000000, 0.000000000000000000 ) ) ;
#6701=FILL_AREA_STYLE ('',( #4211 ) ) ;
#6703=CARTESIAN_POINT ( 'NONE',  ( 32.64999999999997726, 30.00000000000001421, 4.599999999999997868 ) ) ;
#6721=FACE_OUTER_BOUND ( 'NONE', #861, .T. ) ;
#6738=PLANE ( 'NONE',  #77 ) ;
#6740=VECTOR ( 'NONE', #4073, 1000.000000000000000 ) ;
#6743=LINE ( 'NONE', #512, #3859 ) ;
#6746=DIRECTION ( 'NONE',  ( -0.000000000000000000, -0.000000000000000000, 1.000000000000000000 ) ) ;
#6755=DIRECTION ( 'NONE',  ( -0.000000000000000000, -0.000000000000000000, 1.000000000000000000 ) ) ;
#6762=CIRCLE ( 'NONE', #6623, 4.999999999999997335 ) ;
#6782=CARTESIAN_POINT ( 'NONE',  ( 40.00000000000000711, -39.99999999999999289, 10.00000000000000000 ) ) ;
#6795=DIRECTION ( 'NONE',  ( 1.000000000000000000, 0.000000000000000000, 0.000000000000000000 ) ) ;
#6798=EDGE_CURVE ( 'NONE', #1855, #6979, #7133, .T. ) ;
#6803=DIRECTION ( 'NONE',  ( -0.000000000000000000, -0.000000000000000000, 1.000000000000000000 ) ) ;
#6818=EDGE_CURVE ( 'NONE', #191, #4437, #4742, .T. ) ;
#6822=VERTEX_POINT ( 'NONE', #975 ) ;
#6830=ORIENTED_EDGE ( 'NONE', *, *, #5611, .T. ) ;
#6831=ORIENTED_EDGE ( 'NONE', *, *, #5976, .T. ) ;
#6832=ADVANCED_BREP_SHAPE_REPRESENTATION ( '', ( #6657, #1587 ), #517 ) ;
#6834=LINE ( 'NONE', #5685, #652 ) ;
#6844=PLANE ( 'NONE',  #6082 ) ;
#6856=DIRECTION ( 'NONE',  ( 0.000000000000000000, -1.000000000000000000, 0.000000000000000000 ) ) ;
#6857=ADVANCED_FACE ( 'NONE', ( #4438 ), #565, .F. ) ;
#6861=CARTESIAN_POINT ( 'NONE',  ( 40.00000000000000711, -39.99999999999999289, 0.000000000000000000 ) ) ;
#6864=ORIENTED_EDGE ( 'NONE', *, *, #7203, .F. ) ;
#6877=ORIENTED_EDGE ( 'NONE', *, *, #5049, .F. ) ;
#6883=AXIS2_PLACEMENT_3D ( 'NONE', #691, #3238, #2611 ) ;
#6893=CARTESIAN_POINT ( 'NONE',  ( -32.64999999999999858, -29.99999999999999289, 1.734723475976807094E-15 ) ) ;
#6895=AXIS2_PLACEMENT_3D ( 'NONE', #8087, #2314, #437 ) ;
#6898=AXIS2_PLACEMENT_3D ( 'NONE', #1636, #4163, #6692 ) ;
#6919=DIRECTION ( 'NONE',  ( 0.000000000000000000, 0.000000000000000000, -1.000000000000000000 ) ) ;
#6934=CARTESIAN_POINT ( 'NONE',  ( -30.00000000000000355, -29.99999999999999289, 4.599999999999997868 ) ) ;
#6960=CARTESIAN_POINT ( 'NONE',  ( 30.00000000000001066, -29.99999999999997868, 1.734723475976807094E-15 ) ) ;
#6963=DIRECTION ( 'NONE',  ( 0.000000000000000000, 0.000000000000000000, -1.000000000000000000 ) ) ;
#6979=VERTEX_POINT ( 'NONE', #4559 ) ;
#6983=CIRCLE ( 'NONE', #6039, 2.650000000000003020 ) ;
#6986=CARTESIAN_POINT ( 'NONE',  ( -39.99999999999999289, -39.99999999999999289, 10.00000000000000000 ) ) ;
#6990=AXIS2_PLACEMENT_3D ( 'NONE', #6173, #8129, #5565 ) ;
#6997=FACE_OUTER_BOUND ( 'NONE', #461, .T. ) ;
#7000=VERTEX_POINT ( 'NONE', #7778 ) ;
#7009=ORIENTED_EDGE ( 'NONE', *, *, #4527, .T. ) ;
#7020=EDGE_CURVE ( 'NONE', #2205, #4530, #5438, .T. ) ;
#7021=AXIS2_PLACEMENT_3D ( 'NONE', #6453, #757, #3312 ) ;
#7040=CARTESIAN_POINT ( 'NONE',  ( -27.34999999999999076, 30.00000000000000711, 4.599999999999997868 ) ) ;
#7045=ADVANCED_FACE ( 'NONE', ( #7667 ), #4594, .T. ) ;
#7046=AXIS2_PLACEMENT_3D ( 'NONE', #2175, #4709, #7238 ) ;
#7047=CARTESIAN_POINT ( 'NONE',  ( 0.000000000000000000, 0.000000000000000000, 18.00000000000000355 ) ) ;
#7050=CARTESIAN_POINT ( 'NONE',  ( -30.00000000000000355, -29.99999999999999289, 4.599999999999997868 ) ) ;
#7051=CYLINDRICAL_SURFACE ( 'NONE', #1745, 4.999999999999993783 ) ;
#7063=ORIENTED_EDGE ( 'NONE', *, *, #2966, .F. ) ;
#7069=DIRECTION ( 'NONE',  ( -0.000000000000000000, -0.000000000000000000, 1.000000000000000000 ) ) ;
#7092=FACE_OUTER_BOUND ( 'NONE', #6299, .T. ) ;
#7107=CARTESIAN_POINT ( 'NONE',  ( -32.64999999999999147, 30.00000000000000711, 10.00000000000000000 ) ) ;
#7114=CYLINDRICAL_SURFACE ( 'NONE', #4637, 2.649999999999999467 ) ;
#7119=CIRCLE ( 'NONE', #1293, 4.999999999999997335 ) ;
#7125=DIRECTION ( 'NONE',  ( -1.000000000000000000, 0.000000000000000000, 0.000000000000000000 ) ) ;
#7130=VECTOR ( 'NONE', #2027, 1000.000000000000000 ) ;
#7133=CIRCLE ( 'NONE', #5029, 10.00000000000000000 ) ;
#7142=ORIENTED_EDGE ( 'NONE', *, *, #6162, .F. ) ;
#7162=VECTOR ( 'NONE', #4893, 1000.000000000000000 ) ;
#7168=CIRCLE ( 'NONE', #5457, 4.999999999999997335 ) ;
#7181=EDGE_LOOP ( 'NONE', ( #1373, #2165, #7900, #7691 ) ) ;
#7192=ADVANCED_FACE ( 'NONE', ( #4088 ), #7236, .F. ) ;
#7198=LINE ( 'NONE', #7822, #1719 ) ;
#7203=EDGE_CURVE ( 'NONE', #2558, #5625, #4519, .T. ) ;
#7206=AXIS2_PLACEMENT_3D ( 'NONE', #944, #3402, #3489 ) ;
#7227=EDGE_LOOP ( 'NONE', ( #5409, #6095, #7885, #7522 ) ) ;
#7229=CARTESIAN_POINT ( 'NONE',  ( 7.000000000000000000, 8.572527594031473190E-16, 10.00000000000000000 ) ) ;
#7236=CYLINDRICAL_SURFACE ( 'NONE', #5580, 2.649999999999995914 ) ;
#7238=DIRECTION ( 'NONE',  ( 1.000000000000000000, 0.000000000000000000, 0.000000000000000000 ) ) ;
#7240=DIRECTION ( 'NONE',  ( 1.000000000000000000, 0.000000000000000000, 0.000000000000000000 ) ) ;
#7244=DIRECTION ( 'NONE',  ( 0.000000000000000000, 0.000000000000000000, 1.000000000000000000 ) ) ;
#7259=CYLINDRICAL_SURFACE ( 'NONE', #1624, 4.999999999999997335 ) ;
#7272=DIRECTION ( 'NONE',  ( 1.000000000000000000, 0.000000000000000000, 0.000000000000000000 ) ) ;
#7279=CIRCLE ( 'NONE', #2911, 10.00000000000000000 ) ;
#7284=SURFACE_STYLE_FILL_AREA ( #6701 ) ;
#7289=CARTESIAN_POINT ( 'NONE',  ( 0.000000000000000000, 0.000000000000000000, 18.00000000000000355 ) ) ;
#7291=AXIS2_PLACEMENT_3D ( 'NONE', #6518, #6443, #858 ) ;
#7297=DIRECTION ( 'NONE',  ( -0.000000000000000000, -0.000000000000000000, -1.000000000000000000 ) ) ;
#7310=DIRECTION ( 'NONE',  ( -0.000000000000000000, -0.000000000000000000, 1.000000000000000000 ) ) ;
#7340=ORIENTED_EDGE ( 'NONE', *, *, #6483, .T. ) ;
#7348=DIRECTION ( 'NONE',  ( 1.000000000000000000, 0.000000000000000000, 0.000000000000000000 ) ) ;
#7352=ORIENTED_EDGE ( 'NONE', *, *, #6571, .T. ) ;
#7354=ORIENTED_EDGE ( 'NONE', *, *, #5976, .F. ) ;
#7360=ORIENTED_EDGE ( 'NONE', *, *, #7946, .F. ) ;
#7369=ORIENTED_EDGE ( 'NONE', *, *, #5611, .F. ) ;
#7380=ADVANCED_FACE ( 'NONE', ( #2835 ), #326, .F. ) ;
#7381=ORIENTED_EDGE ( 'NONE', *, *, #1274, .T. ) ;
#7385=LINE ( 'NONE', #1703, #3758 ) ;
#7391=ORIENTED_EDGE ( 'NONE', *, *, #2608, .T. ) ;
#7396=DIRECTION ( 'NONE',  ( -0.000000000000000000, -0.000000000000000000, 1.000000000000000000 ) ) ;
#7401=CARTESIAN_POINT ( 'NONE',  ( 0.000000000000000000, 0.000000000000000000, 10.00000000000000000 ) ) ;
#7402=EDGE_LOOP ( 'NONE', ( #3533, #1811 ) ) ;
#7403=EDGE_LOOP ( 'NONE', ( #3253, #1640, #7979, #2193 ) ) ;
#7404=CIRCLE ( 'NONE', #2110, 4.999999999999993783 ) ;
#7452=EDGE_LOOP ( 'NONE', ( #1023, #1385 ) ) ;
#7464=CARTESIAN_POINT ( 'NONE',  ( -30.00000000000000355, -29.99999999999999289, 1.734723475976807094E-15 ) ) ;
#7465=CARTESIAN_POINT ( 'NONE',  ( 40.00000000000000711, 40.00000000000000711, 10.00000000000000000 ) ) ;
#7472=ADVANCED_FACE ( 'NONE', ( #4871 ), #8054, .F. ) ;
#7474=CARTESIAN_POINT ( 'NONE',  ( -7.000000000000000000, 0.000000000000000000, 10.00000000000000000 ) ) ;
#7482=ORIENTED_EDGE ( 'NONE', *, *, #3106, .F. ) ;
#7520=ADVANCED_FACE ( 'NONE', ( #7975 ), #5498, .F. ) ;
#7522=ORIENTED_EDGE ( 'NONE', *, *, #4285, .F. ) ;
#7533=CIRCLE ( 'NONE', #5026, 2.649999999999999467 ) ;
#7536=LINE ( 'NONE', #4468, #1304 ) ;
#7542=AXIS2_PLACEMENT_3D ( 'NONE', #3281, #7297, #5354 ) ;
#7545=VERTEX_POINT ( 'NONE', #1763 ) ;
#7549=FACE_OUTER_BOUND ( 'NONE', #1130, .T. ) ;
#7550=VECTOR ( 'NONE', #7697, 1000.000000000000000 ) ;
#7562=FACE_OUTER_BOUND ( 'NONE', #451, .T. ) ;
#7567=EDGE_LOOP ( 'NONE', ( #4010, #387 ) ) ;
#7568=AXIS2_PLACEMENT_3D ( 'NONE', #866, #1508, #7272 ) ;
#7578=LINE ( 'NONE', #7, #4921 ) ;
#7582=AXIS2_PLACEMENT_3D ( 'NONE', #4022, #4750, #7125 ) ;
#7589=FACE_BOUND ( 'NONE', #1252, .T. ) ;
#7592=DIRECTION ( 'NONE',  ( -0.000000000000000000, -0.000000000000000000, 1.000000000000000000 ) ) ;
#7598=DIRECTION ( 'NONE',  ( -0.000000000000000000, -0.000000000000000000, 1.000000000000000000 ) ) ;
#7605=CARTESIAN_POINT ( 'NONE',  ( 24.99999999999998224, 30.00000000000001421, 10.00000000000000000 ) ) ;
#7606=DIRECTION ( 'NONE',  ( 1.000000000000000000, 0.000000000000000000, 0.000000000000000000 ) ) ;
#7626=DIRECTION ( 'NONE',  ( -0.000000000000000000, -0.000000000000000000, 1.000000000000000000 ) ) ;
#7633=FACE_BOUND ( 'NONE', #4256, .T. ) ;
#7638=CARTESIAN_POINT ( 'NONE',  ( 4.999999999999993783, 6.123233995736758394E-16, 5.400000000000002132 ) ) ;
#7640=DIRECTION ( 'NONE',  ( 0.000000000000000000, 0.000000000000000000, -1.000000000000000000 ) ) ;
#7641=SURFACE_STYLE_USAGE ( .BOTH. , #7785 ) ;
#7644=CYLINDRICAL_SURFACE ( 'NONE', #3990, 4.999999999999997335 ) ;
#7649=CARTESIAN_POINT ( 'NONE',  ( 29.99999999999997868, 30.00000000000001421, 1.734723475976807094E-15 ) ) ;
#7652=VECTOR ( 'NONE', #4167, 1000.000000000000000 ) ;
#7656=EDGE_CURVE ( 'NONE', #1494, #4585, #5588, .T. ) ;
#7660=PLANE ( 'NONE',  #245 ) ;
#7667=FACE_OUTER_BOUND ( 'NONE', #41, .T. ) ;
#7675=DIRECTION ( 'NONE',  ( 1.000000000000000000, 0.000000000000000000, 0.000000000000000000 ) ) ;
#7688=ORIENTED_EDGE ( 'NONE', *, *, #4258, .F. ) ;
#7689=MECHANICAL_DESIGN_GEOMETRIC_PRESENTATION_REPRESENTATION('',(#2652),#4966);
#7691=ORIENTED_EDGE ( 'NONE', *, *, #1097, .F. ) ;
#7692=EDGE_CURVE ( 'NONE', #3432, #2115, #7703, .T. ) ;
#7697=DIRECTION ( 'NONE',  ( 1.000000000000000000, 0.000000000000000000, 0.000000000000000000 ) ) ;
#7703=CIRCLE ( 'NONE', #4784, 4.999999999999993783 ) ;
#7704=DIRECTION ( 'NONE',  ( -1.000000000000000000, 0.000000000000000000, 0.000000000000000000 ) ) ;
#7710=EDGE_CURVE ( 'NONE', #5372, #792, #2532, .T. ) ;
#7711=EDGE_CURVE ( 'NONE', #2320, #8100, #5317, .T. ) ;
#7712=DIRECTION ( 'NONE',  ( -0.000000000000000000, -0.000000000000000000, -1.000000000000000000 ) ) ;
#7727=EDGE_CURVE ( 'NONE', #2205, #8175, #7578, .T. ) ;
#7778=CARTESIAN_POINT ( 'NONE',  ( -32.64999999999999147, 30.00000000000000711, 4.599999999999997868 ) ) ;
#7782=EDGE_CURVE ( 'NONE', #792, #5372, #6762, .T. ) ;
#7785=SURFACE_SIDE_STYLE ('',( #2581 ) ) ;
#7800=CARTESIAN_POINT ( 'NONE',  ( -29.99999999999999289, 30.00000000000000711, 10.00000000000000000 ) ) ;
#7808=EDGE_CURVE ( 'NONE', #6822, #2407, #4120, .T. ) ;
#7810=EDGE_LOOP ( 'NONE', ( #5396, #828 ) ) ;
#7813=DIRECTION ( 'NONE',  ( -0.000000000000000000, -0.000000000000000000, 1.000000000000000000 ) ) ;
#7820=AXIS2_PLACEMENT_3D ( 'NONE', #3039, #6856, #1166 ) ;
#7822=CARTESIAN_POINT ( 'NONE',  ( 7.000000000000000000, 8.572527594031473190E-16, 18.00000000000000355 ) ) ;
#7828=CIRCLE ( 'NONE', #7046, 7.000000000000000000 ) ;
#7843=FACE_OUTER_BOUND ( 'NONE', #5746, .T. ) ;
#7849=ADVANCED_FACE ( 'NONE', ( #3439 ), #3519, .F. ) ;
#7884=CARTESIAN_POINT ( 'NONE',  ( 40.00000000000000711, -39.99999999999999289, 10.00000000000000000 ) ) ;
#7885=ORIENTED_EDGE ( 'NONE', *, *, #1940, .T. ) ;
#7892=LINE ( 'NONE', #6656, #1471 ) ;
#7896=SHAPE_REPRESENTATION_RELATIONSHIP ( 'NONE' , 'NONE' ,  #2475, #6832 ) ;
#7898=CARTESIAN_POINT ( 'NONE',  ( -34.99999999999999289, 30.00000000000000711, 4.599999999999997868 ) ) ;
#7900=ORIENTED_EDGE ( 'NONE', *, *, #6539, .F. ) ;
#7910=DIRECTION ( 'NONE',  ( -0.000000000000000000, -0.000000000000000000, 1.000000000000000000 ) ) ;
#7923=CIRCLE ( 'NONE', #3422, 4.999999999999993783 ) ;
#7928=DIRECTION ( 'NONE',  ( 0.000000000000000000, 1.000000000000000000, 0.000000000000000000 ) ) ;
#7932=VECTOR ( 'NONE', #5803, 1000.000000000000000 ) ;
#7936=VECTOR ( 'NONE', #2990, 1000.000000000000000 ) ;
#7940=AXIS2_PLACEMENT_3D ( 'NONE', #5537, #7928, #4919 ) ;
#7946=EDGE_CURVE ( 'NONE', #2115, #2558, #7992, .T. ) ;
#7966=CYLINDRICAL_SURFACE ( 'NONE', #1906, 4.999999999999993783 ) ;
#7975=FACE_OUTER_BOUND ( 'NONE', #2356, .T. ) ;
#7979=ORIENTED_EDGE ( 'NONE', *, *, #7711, .F. ) ;
#7980=DIRECTION ( 'NONE',  ( -1.000000000000000000, 0.000000000000000000, 0.000000000000000000 ) ) ;
#7982=DIRECTION ( 'NONE',  ( -0.000000000000000000, -1.000000000000000000, -0.000000000000000000 ) ) ;
#7992=LINE ( 'NONE', #2225, #4235 ) ;
#7995=CYLINDRICAL_SURFACE ( 'NONE', #6895, 2.649999999999995914 ) ;
#7996=ORIENTED_EDGE ( 'NONE', *, *, #3938, .F. ) ;
#8009=ORIENTED_EDGE ( 'NONE', *, *, #457, .T. ) ;
#8013=ADVANCED_FACE ( 'NONE', ( #7549 ), #1239, .F. ) ;
#8022=EDGE_LOOP ( 'NONE', ( #2120, #6864 ) ) ;
#8029=EDGE_LOOP ( 'NONE', ( #1761, #2765 ) ) ;
#8042=DIRECTION ( 'NONE',  ( 1.000000000000000000, 0.000000000000000000, 0.000000000000000000 ) ) ;
#8049=EDGE_CURVE ( 'NONE', #4530, #2205, #3310, .T. ) ;
#8054=PLANE ( 'NONE',  #7820 ) ;
#8073=CARTESIAN_POINT ( 'NONE',  ( -39.99999999999999289, 40.00000000000000711, 0.000000000000000000 ) ) ;
#8087=CARTESIAN_POINT ( 'NONE',  ( 30.00000000000001066, -29.99999999999997868, 10.00000000000000000 ) ) ;
#8100=VERTEX_POINT ( 'NONE', #7465 ) ;
#8101=AXIS2_PLACEMENT_3D ( 'NONE', #728, #3943, #3868 ) ;
#8111=EDGE_LOOP ( 'NONE', ( #2616, #123, #3018, #777 ) ) ;
#8112=ORIENTED_EDGE ( 'NONE', *, *, #5300, .F. ) ;
#8120=EDGE_CURVE ( 'NONE', #4437, #191, #6501, .T. ) ;
#8125=DIRECTION ( 'NONE',  ( -0.000000000000000000, -0.000000000000000000, -1.000000000000000000 ) ) ;
#8129=DIRECTION ( 'NONE',  ( -0.000000000000000000, -0.000000000000000000, -1.000000000000000000 ) ) ;
#8130=ORIENTED_EDGE ( 'NONE', *, *, #2301, .F. ) ;
#8134=DIRECTION ( 'NONE',  ( 1.000000000000000000, 0.000000000000000000, 0.000000000000000000 ) ) ;
#8138=EDGE_LOOP ( 'NONE', ( #1836, #1540 ) ) ;
#8147=DIRECTION ( 'NONE',  ( 0.000000000000000000, 1.000000000000000000, 0.000000000000000000 ) ) ;
#8160=DIRECTION ( 'NONE',  ( -1.000000000000000000, 0.000000000000000000, 0.000000000000000000 ) ) ;
#8168=CARTESIAN_POINT ( 'NONE',  ( -27.35000000000000497, -29.99999999999999289, 1.734723475976807094E-15 ) ) ;
#8169=DIRECTION ( 'NONE',  ( -0.000000000000000000, -0.000000000000000000, 1.000000000000000000 ) ) ;
#8175=VERTEX_POINT ( 'NONE', #3271 ) ;
#8179=ORIENTED_EDGE ( 'NONE', *, *, #271, .F. ) ;
#8182=EDGE_CURVE ( 'NONE', #708, #6538, #4479, .T. ) ;
#8189=CARTESIAN_POINT ( 'NONE',  ( 0.000000000000000000, 0.000000000000000000, 10.00000000000000000 ) ) ;
ENDSEC;
END-ISO-10303-21;
